ISO-10303-21;
HEADER;
FILE_DESCRIPTION (('STEP AP214'),
    '1' );
FILE_NAME ('hex nut high strength_din_Hexagon Nut DIN 6915 - M16 - S.step',
    '2026-10-09T14:04:53',
    ( '' ),
    ( '' ),
    'SwSTEP 2.0',
    'SolidWorks 2021',
    '' );
FILE_SCHEMA (( 'AUTOMOTIVE_DESIGN' ));
ENDSEC;

DATA;
#6=DIRECTION ( 'NONE',  ( -1.000000000000000000, 0.000000000000000000, 0.000000000000000000 ) ) ;
#21=EDGE_LOOP ( 'NONE', ( #101675, #98426, #15089, #46695 ) ) ;
#250=ORIENTED_EDGE ( 'NONE', *, *, #71544, .T. ) ;
#281=CYLINDRICAL_SURFACE ( 'NONE', #32950, 7.000000000000000000 ) ;
#289=CARTESIAN_POINT ( 'NONE',  ( 0.000000000000000000, 0.000000000000000000, -11.12471428571428689 ) ) ;
#355=EDGE_CURVE ( 'NONE', #17308, #71961, #69604, .T. ) ;
#534=ADVANCED_FACE ( 'NONE', ( #97043 ), #23790, .T. ) ;
#538=CYLINDRICAL_SURFACE ( 'NONE', #78993, 7.000000000000000000 ) ;
#564=EDGE_LOOP ( 'NONE', ( #72953, #38325, #11887, #25764 ) ) ;
#580=CIRCLE ( 'NONE', #72902, 8.000000000000000000 ) ;
#680=COLOUR_RGB ( '', 0.09019608, 0.27058824, 0.51372549) ;
#711=AXIS2_PLACEMENT_3D ( 'NONE', #65376, #24423, #49168 ) ;
#867=ORIENTED_EDGE ( 'NONE', *, *, #87061, .F. ) ;
#970=CARTESIAN_POINT ( 'NONE',  ( -1.734723475976807094E-15, 15.58845726811991383, -13.00000000000000000 ) ) ;
#1114=CARTESIAN_POINT ( 'NONE',  ( -13.50000000000000178, -1.317096457811611332, 9.791700870259711920E-16 ) ) ;
#1116=ORIENTED_EDGE ( 'NONE', *, *, #2297, .F. ) ;
#1166=DIRECTION ( 'NONE',  ( -0.000000000000000000, 0.000000000000000000, -1.000000000000000000 ) ) ;
#1167=CIRCLE ( 'NONE', #61511, 8.000000000000000000 ) ;
#1188=CONICAL_SURFACE ( 'NONE', #11533, 13.50000000000000178, 1.047197551196596077 ) ;
#1252=DIRECTION ( 'NONE',  ( 0.000000000000000000, -0.000000000000000000, 1.000000000000000000 ) ) ;
#1262=EDGE_CURVE ( 'NONE', #44273, #68006, #58320, .T. ) ;
#1317=FACE_OUTER_BOUND ( 'NONE', #95853, .T. ) ;
#1382=CARTESIAN_POINT ( 'NONE',  ( -11.28351131189990220, 9.073918974790291969, -12.46553453015540924 ) ) ;
#1416=FACE_OUTER_BOUND ( 'NONE', #84705, .T. ) ;
#1439=ADVANCED_FACE ( 'NONE', ( #19781 ), #39171, .T. ) ;
#1546=ORIENTED_EDGE ( 'NONE', *, *, #12871, .F. ) ;
#1577=MECHANICAL_DESIGN_GEOMETRIC_PRESENTATION_REPRESENTATION('',(#5070),#92830);
#1666=CARTESIAN_POINT ( 'NONE',  ( -2.216488688100141324, -14.30876692738957345, -0.5344654698446129615 ) ) ;
#1709=LINE ( 'NONE', #51860, #59701 ) ;
#1766=VERTEX_POINT ( 'NONE', #37282 ) ;
#1786=EDGE_LOOP ( 'NONE', ( #101838, #61211, #49411, #867 ) ) ;
#1862=CARTESIAN_POINT ( 'NONE',  ( 0.000000000000000000, 0.000000000000000000, -11.82492182392400437 ) ) ;
#1871=ORIENTED_EDGE ( 'NONE', *, *, #41470, .F. ) ;
#1991=CARTESIAN_POINT ( 'NONE',  ( 0.000000000000000000, 0.000000000000000000, -13.00000000000000000 ) ) ;
#2002=CIRCLE ( 'NONE', #65690, 7.000000000000000000 ) ;
#2064=PLANE ( 'NONE',  #3939 ) ;
#2075=CARTESIAN_POINT ( 'NONE',  ( -13.50000000000000000, -7.794228634059985339, -11.79422863405993382 ) ) ;
#2080=EDGE_CURVE ( 'NONE', #1766, #79700, #61601, .T. ) ;
#2098=EDGE_CURVE ( 'NONE', #39498, #91936, #92694, .T. ) ;
#2118=ORIENTED_EDGE ( 'NONE', *, *, #32107, .F. ) ;
#2284=DIRECTION ( 'NONE',  ( 0.000000000000000000, 0.000000000000000000, 1.000000000000000000 ) ) ;
#2297=EDGE_CURVE ( 'NONE', #100438, #44273, #90998, .T. ) ;
#2339=LINE ( 'NONE', #61687, #89177 ) ;
#2391=DIRECTION ( 'NONE',  ( 0.000000000000000000, 0.000000000000000000, 1.000000000000000000 ) ) ;
#2472=PRODUCT_DEFINITION_CONTEXT ( 'detailed design', #67293, 'design' ) ;
#2480=CARTESIAN_POINT ( 'NONE',  ( 8.000000000000000000, 9.797174393178825657E-16, -9.274828571428571422 ) ) ;
#2678=VECTOR ( 'NONE', #97428, 1000.000000000000000 ) ;
#2767=AXIS2_PLACEMENT_3D ( 'NONE', #31671, #31150, #97421 ) ;
#2796=DIRECTION ( 'NONE',  ( -0.000000000000000000, 0.000000000000000000, -1.000000000000000000 ) ) ;
#2886=VERTEX_POINT ( 'NONE', #36906 ) ;
#2978=AXIS2_PLACEMENT_3D ( 'NONE', #34068, #74474, #74998 ) ;
#3002=EDGE_LOOP ( 'NONE', ( #92647, #32866, #64656, #29676 ) ) ;
#3005=CARTESIAN_POINT ( 'NONE',  ( -7.899999792244740249, 11.02739026146940660, -13.00000000000001066 ) ) ;
#3029=ORIENTED_EDGE ( 'NONE', *, *, #79397, .F. ) ;
#3078=( LENGTH_UNIT ( ) NAMED_UNIT ( * ) SI_UNIT ( .MILLI., .METRE. ) );
#3088=CIRCLE ( 'NONE', #102955, 7.000000000000000000 ) ;
#3116=VECTOR ( 'NONE', #106742, 1000.000000000000000 ) ;
#3123=AXIS2_PLACEMENT_3D ( 'NONE', #15592, #80854, #23720 ) ;
#3169=CARTESIAN_POINT ( 'NONE',  ( 0.000000000000000000, 0.000000000000000000, -7.424942857142857733 ) ) ;
#3183=AXIS2_PLACEMENT_3D ( 'NONE', #25997, #76609, #17337 ) ;
#3210=EDGE_LOOP ( 'NONE', ( #10478, #57298, #37512, #1546 ) ) ;
#3265=EDGE_LOOP ( 'NONE', ( #22993, #29012, #78146, #84988 ) ) ;
#3275=EDGE_CURVE ( 'NONE', #84222, #25443, #53646, .T. ) ;
#3299=CARTESIAN_POINT ( 'NONE',  ( 7.322849800245818663, 11.36060796471277889, 7.896605822936082213E-15 ) ) ;
#3302=ORIENTED_EDGE ( 'NONE', *, *, #4195, .T. ) ;
#3372=EDGE_CURVE ( 'NONE', #58364, #25443, #76911, .T. ) ;
#3430=VERTEX_POINT ( 'NONE', #72682 ) ;
#3475=VERTEX_POINT ( 'NONE', #75801 ) ;
#3555=VERTEX_POINT ( 'NONE', #84964 ) ;
#3675=DIRECTION ( 'NONE',  ( -1.000000000000000000, 0.000000000000000000, 0.000000000000000000 ) ) ;
#3748=CARTESIAN_POINT ( 'NONE',  ( 8.000000000000000000, 9.797174393178825657E-16, -11.12471428571428689 ) ) ;
#3753=DIRECTION ( 'NONE',  ( -1.000000000000000000, 0.000000000000000000, 0.000000000000000000 ) ) ;
#3837=AXIS2_PLACEMENT_3D ( 'NONE', #75170, #8850, #41754 ) ;
#3843=DIRECTION ( 'NONE',  ( 0.000000000000000000, 0.000000000000000000, 1.000000000000000000 ) ) ;
#3854=VERTEX_POINT ( 'NONE', #10267 ) ;
#3939=AXIS2_PLACEMENT_3D ( 'NONE', #970, #66821, #9622 ) ;
#3999=FACE_OUTER_BOUND ( 'NONE', #30085, .T. ) ;
#4021=FACE_OUTER_BOUND ( 'NONE', #99597, .T. ) ;
#4175=CARTESIAN_POINT ( 'NONE',  ( -6.900000000000000355, 8.450062914116737647E-16, -0.7702282920306786629 ) ) ;
#4195=EDGE_CURVE ( 'NONE', #50869, #52643, #85711, .T. ) ;
#4358=CARTESIAN_POINT ( 'NONE',  ( 7.898269865231972275, 11.02838903529590731, -0.02849990174189836675 ) ) ;
#4399=LINE ( 'NONE', #12471, #85192 ) ;
#4531=EDGE_CURVE ( 'NONE', #9380, #74189, #58037, .T. ) ;
#4548=CARTESIAN_POINT ( 'NONE',  ( 0.000000000000000000, 0.000000000000000000, -7.424942857142857733 ) ) ;
#4619=CARTESIAN_POINT ( 'NONE',  ( 2.216488688100098248, 14.30876692738955924, -12.46553453015539503 ) ) ;
#4672=EDGE_LOOP ( 'NONE', ( #81577, #3302, #69412, #5799 ) ) ;
#4727=ORIENTED_EDGE ( 'NONE', *, *, #79110, .F. ) ;
#4750=EDGE_LOOP ( 'NONE', ( #48596, #83360, #63962, #13891 ) ) ;
#4776=CARTESIAN_POINT ( 'NONE',  ( 2.216488688100095583, 14.30876692738956102, -0.5344654698446031915 ) ) ;
#4796=EDGE_CURVE ( 'NONE', #3475, #79592, #58588, .T. ) ;
#5009=CARTESIAN_POINT ( 'NONE',  ( 6.750000000000016875, -11.69134295108991495, 0.000000000000000000 ) ) ;
#5048=CARTESIAN_POINT ( 'NONE',  ( 6.750000000000016875, -11.69134295108991495, -13.00000000000000000 ) ) ;
#5052=LINE ( 'NONE', #54105, #70862 ) ;
#5070=STYLED_ITEM ( 'NONE', ( #18772 ), #90584 ) ;
#5139=ORIENTED_EDGE ( 'NONE', *, *, #32645, .F. ) ;
#5223=CONICAL_SURFACE ( 'NONE', #13750, 13.50000000000000178, 1.047197551196596077 ) ;
#5304=CYLINDRICAL_SURFACE ( 'NONE', #35947, 7.000000000000000000 ) ;
#5313=CARTESIAN_POINT ( 'NONE',  ( 5.600000207755286397, 12.35529564071043040, 7.521652571618187011E-15 ) ) ;
#5575=DIRECTION ( 'NONE',  ( -1.000000000000000000, 0.000000000000000000, 0.000000000000000000 ) ) ;
#5616=CARTESIAN_POINT ( 'NONE',  ( -3.601501433546143538E-16, 15.58845726811991206, -13.00000000000000000 ) ) ;
#5704=DIRECTION ( 'NONE',  ( -0.8191520442889884679, 1.003171929053520679E-16, 0.5735764363510509334 ) ) ;
#5719=DIRECTION ( 'NONE',  ( -0.000000000000000000, -0.000000000000000000, -1.000000000000000000 ) ) ;
#5779=CARTESIAN_POINT ( 'NONE',  ( -8.000000000000000000, 0.000000000000000000, -3.725171428571429022 ) ) ;
#5791=DIRECTION ( 'NONE',  ( -1.000000000000000000, 0.000000000000000000, 0.000000000000000000 ) ) ;
#5799=ORIENTED_EDGE ( 'NONE', *, *, #61995, .F. ) ;
#5807=CARTESIAN_POINT ( 'NONE',  ( 7.000000000000000000, 0.000000000000000000, -13.00000000000000000 ) ) ;
#5858=DIRECTION ( 'NONE',  ( 0.000000000000000000, 0.000000000000000000, -1.000000000000000000 ) ) ;
#5893=ADVANCED_FACE ( 'NONE', ( #31243 ), #58368, .T. ) ;
#5973=CARTESIAN_POINT ( 'NONE',  ( 0.000000000000000000, 0.000000000000000000, -5.575057142857143155 ) ) ;
#6027=LINE ( 'NONE', #78331, #28760 ) ;
#6222=CIRCLE ( 'NONE', #11375, 13.50000000000000000 ) ;
#6309=DIRECTION ( 'NONE',  ( -0.8660254037844378194, 0.5000000000000013323, 0.000000000000000000 ) ) ;
#6472=CARTESIAN_POINT ( 'NONE',  ( -8.000000000000000000, 0.000000000000000000, -9.274828571428571422 ) ) ;
#6513=EDGE_CURVE ( 'NONE', #31665, #91936, #51890, .T. ) ;
#6634=EDGE_LOOP ( 'NONE', ( #83871, #95022, #1871, #55637 ) ) ;
#6659=CARTESIAN_POINT ( 'NONE',  ( 6.750000000000017764, 11.69134295108991317, -13.00000000000000000 ) ) ;
#6815=VERTEX_POINT ( 'NONE', #6659 ) ;
#6823=DIRECTION ( 'NONE',  ( -0.000000000000000000, -0.000000000000000000, -1.000000000000000000 ) ) ;
#6905=ADVANCED_FACE ( 'NONE', ( #15286 ), #95982, .F. ) ;
#7021=VECTOR ( 'NONE', #65313, 1000.000000000000000 ) ;
#7069=DIRECTION ( 'NONE',  ( 1.000000000000000000, 0.000000000000000000, 0.000000000000000000 ) ) ;
#7114=CARTESIAN_POINT ( 'NONE',  ( 13.50000000000000533, 0.6589394956329788222, -13.00000000000000000 ) ) ;
#7125=VERTEX_POINT ( 'NONE', #106140 ) ;
#7144=EDGE_CURVE ( 'NONE', #64475, #3854, #25408, .T. ) ;
#7157=LINE ( 'NONE', #105856, #20275 ) ;
#7208=CARTESIAN_POINT ( 'NONE',  ( -7.000000000000000000, 8.572527594031471218E-16, -8.574621033218877031 ) ) ;
#7349=ORIENTED_EDGE ( 'NONE', *, *, #72208, .F. ) ;
#7438=DIRECTION ( 'NONE',  ( -1.000000000000000000, 0.000000000000000000, 0.000000000000000000 ) ) ;
#7473=ORIENTED_EDGE ( 'NONE', *, *, #30324, .F. ) ;
#7548=DIRECTION ( 'NONE',  ( -0.8191520442889974607, 0.000000000000000000, -0.5735764363510380548 ) ) ;
#7634=AXIS2_PLACEMENT_3D ( 'NONE', #5973, #30289, #64759 ) ;
#7665=AXIS2_PLACEMENT_3D ( 'NONE', #3169, #100262, #59291 ) ;
#7838=CARTESIAN_POINT ( 'NONE',  ( 13.50000000000000178, 3.304540750553671469, -0.2220019300505709781 ) ) ;
#7930=ADVANCED_FACE ( 'NONE', ( #13031 ), #34777, .F. ) ;
#7931=ORIENTED_EDGE ( 'NONE', *, *, #60282, .F. ) ;
#7938=EDGE_CURVE ( 'NONE', #34348, #64513, #2002, .T. ) ;
#7974=AXIS2_PLACEMENT_3D ( 'NONE', #20395, #65563, #97925 ) ;
#8012=ADVANCED_FACE ( 'NONE', ( #16763 ), #103640, .T. ) ;
#8105=( NAMED_UNIT ( * ) SI_UNIT ( $, .STERADIAN. ) SOLID_ANGLE_UNIT ( ) );
#8135=CONICAL_SURFACE ( 'NONE', #102943, 8.000000000000000000, 0.9599310885968911355 ) ;
#8176=ADVANCED_FACE ( 'NONE', ( #18936 ), #93098, .T. ) ;
#8184=CARTESIAN_POINT ( 'NONE',  ( 13.50000000000000355, -7.794228634059974681, -13.00000000000000000 ) ) ;
#8238=EDGE_LOOP ( 'NONE', ( #86373, #25861, #26791, #86002 ) ) ;
#8310=AXIS2_PLACEMENT_3D ( 'NONE', #62683, #53520, #46488 ) ;
#8324=FACE_OUTER_BOUND ( 'NONE', #26455, .T. ) ;
#8406=EDGE_CURVE ( 'NONE', #18742, #9380, #22101, .T. ) ;
#8438=CARTESIAN_POINT ( 'NONE',  ( 0.000000000000000000, 0.000000000000000000, 0.000000000000000000 ) ) ;
#8567=DIRECTION ( 'NONE',  ( -0.000000000000000000, -0.000000000000000000, 1.000000000000000000 ) ) ;
#8645=VECTOR ( 'NONE', #34236, 1000.000000000000000 ) ;
#8660=EDGE_LOOP ( 'NONE', ( #86905, #26600, #39392, #66116, #14813, #42557 ) ) ;
#8799=CARTESIAN_POINT ( 'NONE',  ( 7.981862520314372489, 0.000000000000000000, -0.01269999999999830292 ) ) ;
#8850=DIRECTION ( 'NONE',  ( 0.000000000000000000, 0.000000000000000000, 1.000000000000000000 ) ) ;
#8894=DIRECTION ( 'NONE',  ( -0.000000000000000000, -0.000000000000000000, -1.000000000000000000 ) ) ;
#8982=CARTESIAN_POINT ( 'NONE',  ( 0.000000000000000000, 0.000000000000000000, -2.575493252495433261 ) ) ;
#8987=CARTESIAN_POINT ( 'NONE',  ( 7.899999792244757124, -11.02739026146943857, -1.226164894445325171E-14 ) ) ;
#8988=DIRECTION ( 'NONE',  ( -0.000000000000000000, -0.000000000000000000, -1.000000000000000000 ) ) ;
#9037=AXIS2_PLACEMENT_3D ( 'NONE', #28148, #3843, #75592 ) ;
#9056=CARTESIAN_POINT ( 'NONE',  ( 8.000000000000000000, 9.797174393178825657E-16, -7.424942857142857733 ) ) ;
#9061=ORIENTED_EDGE ( 'NONE', *, *, #23207, .F. ) ;
#9105=CARTESIAN_POINT ( 'NONE',  ( -7.898269865231990039, -11.02838903529593573, -12.97150009825808503 ) ) ;
#9226=DIRECTION ( 'NONE',  ( -0.000000000000000000, -0.000000000000000000, 1.000000000000000000 ) ) ;
#9299=CARTESIAN_POINT ( 'NONE',  ( 8.000000000000000000, 0.000000000000000000, -25.03750572909317285 ) ) ;
#9380=VERTEX_POINT ( 'NONE', #70824 ) ;
#9450=ORIENTED_EDGE ( 'NONE', *, *, #94664, .F. ) ;
#9465=FACE_OUTER_BOUND ( 'NONE', #24791, .T. ) ;
#9519=EDGE_LOOP ( 'NONE', ( #21705, #16002, #69929, #38654, #84351, #9450 ) ) ;
#9557=( NAMED_UNIT ( * ) PLANE_ANGLE_UNIT ( ) SI_UNIT ( $, .RADIAN. ) );
#9583=CARTESIAN_POINT ( 'NONE',  ( -5.601730134768055258, 12.35429686688392259, -0.02849990174189845002 ) ) ;
#9606=CARTESIAN_POINT ( 'NONE',  ( -13.50000000000000000, 7.794228634059985339, -11.79422863405993382 ) ) ;
#9622=DIRECTION ( 'NONE',  ( -1.000000000000000000, 0.000000000000000000, 0.000000000000000000 ) ) ;
#9662=DIRECTION ( 'NONE',  ( 1.000000000000000000, 0.000000000000000000, 0.000000000000000000 ) ) ;
#9672=B_SPLINE_CURVE_WITH_KNOTS ( 'NONE', 3,
 ( #55015, #89004, #38866, #71732, #47986, #39402 ),
 .UNSPECIFIED., .F., .F.,
 ( 4, 2, 4 ),
 ( 0.01390592816464533005, 0.01784842065628997748, 0.02179091314793462145 ),
 .UNSPECIFIED. ) ;
#9759=VECTOR ( 'NONE', #42929, 1000.000000000000000 ) ;
#9762=ADVANCED_FACE ( 'NONE', ( #16032 ), #98014, .T. ) ;
#9899=CARTESIAN_POINT ( 'NONE',  ( 9.601913782316092494, 10.04478976116411815, -12.77952306666690241 ) ) ;
#9933=FACE_OUTER_BOUND ( 'NONE', #13728, .T. ) ;
#9934=CARTESIAN_POINT ( 'NONE',  ( -6.158268339717665185E-14, -15.58845726811991739, -11.79422863405993382 ) ) ;
#10022=CARTESIAN_POINT ( 'NONE',  ( 7.000000000000000000, 0.000000000000000000, -13.00000000000000000 ) ) ;
#10031=EDGE_CURVE ( 'NONE', #26535, #58364, #51490, .T. ) ;
#10101=SURFACE_STYLE_USAGE ( .BOTH. , #100699 ) ;
#10143=CARTESIAN_POINT ( 'NONE',  ( -6.750000000000018652, 11.69134295108991317, -13.00000000000000000 ) ) ;
#10200=CYLINDRICAL_SURFACE ( 'NONE', #44365, 7.000000000000000000 ) ;
#10204=EDGE_CURVE ( 'NONE', #16577, #99841, #31427, .T. ) ;
#10248=CARTESIAN_POINT ( 'NONE',  ( -13.50000000000000178, 0.000000000000000000, 0.000000000000000000 ) ) ;
#10263=CARTESIAN_POINT ( 'NONE',  ( -8.673617379884035472E-16, 15.58845726811991561, -1.205771365940065953 ) ) ;
#10267=CARTESIAN_POINT ( 'NONE',  ( -7.000000000000000000, 8.572527594031471218E-16, -8.125150395352576993 ) ) ;
#10335=CIRCLE ( 'NONE', #49905, 7.000000000000000000 ) ;
#10379=ORIENTED_EDGE ( 'NONE', *, *, #55082, .F. ) ;
#10396=ADVANCED_FACE ( 'NONE', ( #9933 ), #71038, .F. ) ;
#10478=ORIENTED_EDGE ( 'NONE', *, *, #26063, .F. ) ;
#10488=CIRCLE ( 'NONE', #103501, 7.000000000000000000 ) ;
#10505=DIRECTION ( 'NONE',  ( -0.000000000000000000, -0.000000000000000000, -1.000000000000000000 ) ) ;
#10556=CARTESIAN_POINT ( 'NONE',  ( -6.750000000000018652, 11.69134295108991317, -13.00000000000000000 ) ) ;
#10726=CYLINDRICAL_SURFACE ( 'NONE', #49876, 7.000000000000000000 ) ;
#10728=AXIS2_PLACEMENT_3D ( 'NONE', #14983, #57033, #47878 ) ;
#10794=CARTESIAN_POINT ( 'NONE',  ( 13.50000000000000533, -7.794228634059982674, -11.79422863405993382 ) ) ;
#10849=EDGE_CURVE ( 'NONE', #79592, #74189, #1709, .T. ) ;
#10882=AXIS2_PLACEMENT_3D ( 'NONE', #16051, #17137, #81301 ) ;
#10929=EDGE_LOOP ( 'NONE', ( #35569, #97882, #65461 ) ) ;
#10948=DIRECTION ( 'NONE',  ( -1.000000000000000000, 0.000000000000000000, 0.000000000000000000 ) ) ;
#10973=FACE_OUTER_BOUND ( 'NONE', #42430, .T. ) ;
#11007=LINE ( 'NONE', #68756, #54162 ) ;
#11125=CARTESIAN_POINT ( 'NONE',  ( 0.000000000000000000, 0.000000000000000000, -12.97459999999999525 ) ) ;
#11213=FACE_OUTER_BOUND ( 'NONE', #70731, .T. ) ;
#11255=FACE_OUTER_BOUND ( 'NONE', #60077, .T. ) ;
#11297=ORIENTED_EDGE ( 'NONE', *, *, #106064, .T. ) ;
#11375=AXIS2_PLACEMENT_3D ( 'NONE', #64849, #30926, #14683 ) ;
#11384=ORIENTED_EDGE ( 'NONE', *, *, #38114, .F. ) ;
#11431=EDGE_CURVE ( 'NONE', #15319, #3854, #11007, .T. ) ;
#11451=ADVANCED_FACE ( 'NONE', ( #76283 ), #86934, .F. ) ;
#11517=CARTESIAN_POINT ( 'NONE',  ( 1.101454001169991148, -14.95253250404446632, -12.16137996778338781 ) ) ;
#11533=AXIS2_PLACEMENT_3D ( 'NONE', #46897, #79803, #38831 ) ;
#11660=ORIENTED_EDGE ( 'NONE', *, *, #51143, .F. ) ;
#11850=DIRECTION ( 'NONE',  ( -0.000000000000000000, -0.000000000000000000, 1.000000000000000000 ) ) ;
#11887=ORIENTED_EDGE ( 'NONE', *, *, #87061, .T. ) ;
#11912=CARTESIAN_POINT ( 'NONE',  ( 9.036570576874952465, 10.37119081301008094, -0.1387913946425728406 ) ) ;
#11968=ORIENTED_EDGE ( 'NONE', *, *, #79110, .T. ) ;
#12053=ADVANCED_FACE ( 'NONE', ( #8324 ), #67303, .F. ) ;
#12060=CARTESIAN_POINT ( 'NONE',  ( -6.158268339717665185E-14, -15.58845726811991739, -11.79422863405993382 ) ) ;
#12091=DIRECTION ( 'NONE',  ( -0.000000000000000000, -0.000000000000000000, 1.000000000000000000 ) ) ;
#12105=DIRECTION ( 'NONE',  ( -1.000000000000000000, 0.000000000000000000, 0.000000000000000000 ) ) ;
#12143=APPLICATION_CONTEXT ( 'automotive_design' ) ;
#12198=ORIENTED_EDGE ( 'NONE', *, *, #69028, .F. ) ;
#12200=CARTESIAN_POINT ( 'NONE',  ( -7.000000000000000000, 8.572527594031473190E-16, -2.575493252495433261 ) ) ;
#12215=CONICAL_SURFACE ( 'NONE', #20912, 7.000000000000000000, 0.9599310885968753704 ) ;
#12256=ORIENTED_EDGE ( 'NONE', *, *, #91415, .T. ) ;
#12267=CARTESIAN_POINT ( 'NONE',  ( -13.50000000000000178, 6.533945317241069084, -0.8419589098297682872 ) ) ;
#12471=CARTESIAN_POINT ( 'NONE',  ( -7.000000000000000000, 8.572527594031471218E-16, -13.00000000000000000 ) ) ;
#12479=AXIS2_PLACEMENT_3D ( 'NONE', #14821, #89792, #15895 ) ;
#12490=DIRECTION ( 'NONE',  ( -0.000000000000000000, -0.000000000000000000, -1.000000000000000000 ) ) ;
#12622=AXIS2_PLACEMENT_3D ( 'NONE', #78715, #46883, #53406 ) ;
#12652=CIRCLE ( 'NONE', #45413, 13.50000000000000000 ) ;
#12717=CARTESIAN_POINT ( 'NONE',  ( -6.750000000000018652, 11.69134295108991317, 0.000000000000000000 ) ) ;
#12871=EDGE_CURVE ( 'NONE', #15319, #47413, #64727, .T. ) ;
#13031=FACE_OUTER_BOUND ( 'NONE', #50927, .T. ) ;
#13075=DIRECTION ( 'NONE',  ( -1.000000000000000000, 0.000000000000000000, 0.000000000000000000 ) ) ;
#13283=CIRCLE ( 'NONE', #2978, 13.50000000000000178 ) ;
#13307=LINE ( 'NONE', #4175, #98175 ) ;
#13312=CYLINDRICAL_SURFACE ( 'NONE', #94317, 7.000000000000000000 ) ;
#13381=DIRECTION ( 'NONE',  ( -0.000000000000000000, -0.000000000000000000, 1.000000000000000000 ) ) ;
#13433=CIRCLE ( 'NONE', #54789, 7.000000000000000000 ) ;
#13508=CIRCLE ( 'NONE', #15284, 7.000000000000000000 ) ;
#13524=ADVANCED_FACE ( 'NONE', ( #79082 ), #87036, .F. ) ;
#13554=ORIENTED_EDGE ( 'NONE', *, *, #2080, .F. ) ;
#13599=DIRECTION ( 'NONE',  ( -1.000000000000000000, 0.000000000000000000, 0.000000000000000000 ) ) ;
#13657=ORIENTED_EDGE ( 'NONE', *, *, #36375, .T. ) ;
#13683=SHAPE_DEFINITION_REPRESENTATION ( #45916, #74292 ) ;
#13728=EDGE_LOOP ( 'NONE', ( #63913, #29247, #61287, #49194 ) ) ;
#13750=AXIS2_PLACEMENT_3D ( 'NONE', #19712, #12091, #36428 ) ;
#13770=AXIS2_PLACEMENT_3D ( 'NONE', #49012, #92141, #100762 ) ;
#13773=DIRECTION ( 'NONE',  ( -0.000000000000000000, -0.000000000000000000, -1.000000000000000000 ) ) ;
#13791=ADVANCED_FACE ( 'NONE', ( #76639 ), #35382, .F. ) ;
#13796=CONICAL_SURFACE ( 'NONE', #22470, 7.000000000000000000, 0.9599310885968753704 ) ;
#13891=ORIENTED_EDGE ( 'NONE', *, *, #59427, .F. ) ;
#13936=FACE_OUTER_BOUND ( 'NONE', #77747, .T. ) ;
#14081=VECTOR ( 'NONE', #7548, 1000.000000000000000 ) ;
#14183=DIRECTION ( 'NONE',  ( -1.000000000000000000, 0.000000000000000000, 0.000000000000000000 ) ) ;
#14229=AXIS2_PLACEMENT_3D ( 'NONE', #39891, #56582, #16668 ) ;
#14287=CARTESIAN_POINT ( 'NONE',  ( -8.000000000000000000, 9.797174393178825657E-16, 3.469446951953614189E-15 ) ) ;
#14299=CARTESIAN_POINT ( 'NONE',  ( -11.28351131189991641, 9.073918974790284864, -0.5344654698445947538 ) ) ;
#14332=CARTESIAN_POINT ( 'NONE',  ( 0.000000000000000000, 0.000000000000000000, -9.274828571428571422 ) ) ;
#14406=VERTEX_POINT ( 'NONE', #36816 ) ;
#14414=AXIS2_PLACEMENT_3D ( 'NONE', #47352, #13381, #29113 ) ;
#14592=PRODUCT ( 'hex nut high strength_din_Hexagon Nut DIN 6915 - M16 - S', 'hex nut high strength_din_Hexagon Nut DIN 6915 - M16 - S', '', ( #29391 ) ) ;
#14608=CARTESIAN_POINT ( 'NONE',  ( 0.000000000000000000, 0.000000000000000000, -0.7256075382097185722 ) ) ;
#14615=CARTESIAN_POINT ( 'NONE',  ( -1.734723475976807094E-15, 15.58845726811991383, 0.000000000000000000 ) ) ;
#14670=ORIENTED_EDGE ( 'NONE', *, *, #92109, .T. ) ;
#14683=DIRECTION ( 'NONE',  ( -1.000000000000000000, 0.000000000000000000, 0.000000000000000000 ) ) ;
#14700=EDGE_CURVE ( 'NONE', #60873, #3475, #90631, .T. ) ;
#14727=ORIENTED_EDGE ( 'NONE', *, *, #80554, .F. ) ;
#14760=AXIS2_PLACEMENT_3D ( 'NONE', #89664, #31454, #72919 ) ;
#14813=ORIENTED_EDGE ( 'NONE', *, *, #19938, .F. ) ;
#14821=CARTESIAN_POINT ( 'NONE',  ( 0.000000000000000000, 0.000000000000000000, -13.00000000000000000 ) ) ;
#14828=DIRECTION ( 'NONE',  ( 0.000000000000000000, 0.000000000000000000, 1.000000000000000000 ) ) ;
#14832=VECTOR ( 'NONE', #94207, 1000.000000000000000 ) ;
#14895=DIRECTION ( 'NONE',  ( -0.8191520442889911324, 1.003171929053523884E-16, 0.5735764363510470476 ) ) ;
#14909=FACE_OUTER_BOUND ( 'NONE', #4750, .T. ) ;
#14983=CARTESIAN_POINT ( 'NONE',  ( 0.000000000000000000, 0.000000000000000000, 0.000000000000000000 ) ) ;
#15004=CARTESIAN_POINT ( 'NONE',  ( -7.000000000000000000, 8.572527594031473190E-16, -0.7256075382097185722 ) ) ;
#15074=DIRECTION ( 'NONE',  ( 0.000000000000000000, 0.000000000000000000, 1.000000000000000000 ) ) ;
#15080=DIRECTION ( 'NONE',  ( -1.000000000000000000, 0.000000000000000000, 0.000000000000000000 ) ) ;
#15089=ORIENTED_EDGE ( 'NONE', *, *, #66692, .F. ) ;
#15099=CARTESIAN_POINT ( 'NONE',  ( 0.000000000000000000, 0.000000000000000000, -8.125150395352576993 ) ) ;
#15118=AXIS2_PLACEMENT_3D ( 'NONE', #14615, #105246, #80417 ) ;
#15133=EDGE_LOOP ( 'NONE', ( #78593, #47327, #32942, #68063 ) ) ;
#15261=DIRECTION ( 'NONE',  ( 0.8191520442889884679, 0.000000000000000000, 0.5735764363510509334 ) ) ;
#15284=AXIS2_PLACEMENT_3D ( 'NONE', #66220, #67305, #12105 ) ;
#15286=FACE_OUTER_BOUND ( 'NONE', #6634, .T. ) ;
#15304=CONICAL_SURFACE ( 'NONE', #65276, 13.50000000000000178, 1.047197551196596077 ) ;
#15319=VERTEX_POINT ( 'NONE', #7208 ) ;
#15325=CONICAL_SURFACE ( 'NONE', #60103, 8.000000000000000000, 0.9599310885968911355 ) ;
#15370=B_SPLINE_CURVE_WITH_KNOTS ( 'NONE', 3,
 ( #103810, #29955, #62839, #95730, #38571, #97838 ),
 .UNSPECIFIED., .F., .F.,
 ( 4, 2, 4 ),
 ( 2.380729205335813291E-07, 0.003943479449179693175, 0.007886720825438852528 ),
 .UNSPECIFIED. ) ;
#15408=CARTESIAN_POINT ( 'NONE',  ( 13.50000000000000711, 5.257130651325589099, -0.5389759092231705129 ) ) ;
#15436=EDGE_CURVE ( 'NONE', #35268, #91137, #89081, .T. ) ;
#15463=AXIS2_PLACEMENT_3D ( 'NONE', #46789, #62983, #5791 ) ;
#15592=CARTESIAN_POINT ( 'NONE',  ( 0.000000000000000000, 0.000000000000000000, -13.00000000000000000 ) ) ;
#15681=CARTESIAN_POINT ( 'NONE',  ( 0.000000000000000000, 0.000000000000000000, -13.00000000000000000 ) ) ;
#15817=DIRECTION ( 'NONE',  ( 0.000000000000000000, 0.000000000000000000, 1.000000000000000000 ) ) ;
#15871=DIRECTION ( 'NONE',  ( 1.000000000000000000, 0.000000000000000000, 0.000000000000000000 ) ) ;
#15895=DIRECTION ( 'NONE',  ( 1.000000000000000000, 0.000000000000000000, 0.000000000000000000 ) ) ;
#16002=ORIENTED_EDGE ( 'NONE', *, *, #29366, .T. ) ;
#16016=VECTOR ( 'NONE', #84064, 999.9999999999998863 ) ;
#16032=FACE_OUTER_BOUND ( 'NONE', #9519, .T. ) ;
#16051=CARTESIAN_POINT ( 'NONE',  ( 0.000000000000000000, 0.000000000000000000, -13.00000000000000000 ) ) ;
#16053=DIRECTION ( 'NONE',  ( 0.000000000000000000, 0.000000000000000000, 1.000000000000000000 ) ) ;
#16059=CIRCLE ( 'NONE', #47079, 13.50000000000000000 ) ;
#16157=ORIENTED_EDGE ( 'NONE', *, *, #50687, .T. ) ;
#16202=SURFACE_STYLE_USAGE ( .BOTH. , #90097 ) ;
#16311=ORIENTED_EDGE ( 'NONE', *, *, #355, .T. ) ;
#16460=DIRECTION ( 'NONE',  ( -1.000000000000000000, 0.000000000000000000, 0.000000000000000000 ) ) ;
#16577=VERTEX_POINT ( 'NONE', #81432 ) ;
#16648=CIRCLE ( 'NONE', #47666, 7.000000000000000000 ) ;
#16666=FACE_OUTER_BOUND ( 'NONE', #46662, .T. ) ;
#16668=DIRECTION ( 'NONE',  ( 1.000000000000000000, 0.000000000000000000, 0.000000000000000000 ) ) ;
#16763=FACE_OUTER_BOUND ( 'NONE', #101922, .T. ) ;
#16805=CARTESIAN_POINT ( 'NONE',  ( -13.50000000000000000, -7.794228634059985339, -1.205771365940065953 ) ) ;
#16819=CARTESIAN_POINT ( 'NONE',  ( 13.50000000000000533, 5.257130651325587323, -12.46102409077683326 ) ) ;
#16831=AXIS2_PLACEMENT_3D ( 'NONE', #100637, #52086, #76895 ) ;
#16894=DIRECTION ( 'NONE',  ( 1.000000000000000000, 0.000000000000000000, 0.000000000000000000 ) ) ;
#17108=CARTESIAN_POINT ( 'NONE',  ( 0.000000000000000000, 0.000000000000000000, -5.575057142857143155 ) ) ;
#17137=DIRECTION ( 'NONE',  ( 0.000000000000000000, 0.000000000000000000, 1.000000000000000000 ) ) ;
#17206=CYLINDRICAL_SURFACE ( 'NONE', #41017, 8.000000000000000000 ) ;
#17246=DIRECTION ( 'NONE',  ( 0.000000000000000000, 0.000000000000000000, -1.000000000000000000 ) ) ;
#17308=VERTEX_POINT ( 'NONE', #21409 ) ;
#17318=CARTESIAN_POINT ( 'NONE',  ( 0.000000000000000000, 0.000000000000000000, -6.724735318933162453 ) ) ;
#17330=DIRECTION ( 'NONE',  ( 0.000000000000000000, 0.000000000000000000, 1.000000000000000000 ) ) ;
#17337=DIRECTION ( 'NONE',  ( -1.000000000000000000, 3.552713678800500929E-15, 0.000000000000000000 ) ) ;
#17349=ORIENTED_EDGE ( 'NONE', *, *, #90558, .T. ) ;
#17408=VERTEX_POINT ( 'NONE', #20910 ) ;
#17426=CARTESIAN_POINT ( 'NONE',  ( 0.000000000000000000, 0.000000000000000000, -8.125150395352576993 ) ) ;
#17437=DIRECTION ( 'NONE',  ( -0.000000000000000000, -0.000000000000000000, 1.000000000000000000 ) ) ;
#17494=B_SPLINE_CURVE_WITH_KNOTS ( 'NONE', 3,
 ( #30717, #63059, #78687, #87868, #54940, #53886, #88399, #37756 ),
 .UNSPECIFIED., .F., .F.,
 ( 4, 2, 2, 4 ),
 ( 0.007886720825438791813, 0.009850969036564004647, 0.01181521724768921922, 0.01574371366993964488 ),
 .UNSPECIFIED. ) ;
#17507=EDGE_CURVE ( 'NONE', #14406, #7125, #28182, .T. ) ;
#17520=ORIENTED_EDGE ( 'NONE', *, *, #38184, .T. ) ;
#17530=DIRECTION ( 'NONE',  ( 0.000000000000000000, 0.000000000000000000, 1.000000000000000000 ) ) ;
#17570=DIRECTION ( 'NONE',  ( -0.000000000000000000, -0.000000000000000000, -1.000000000000000000 ) ) ;
#17617=ORIENTED_EDGE ( 'NONE', *, *, #2098, .T. ) ;
#17686=EDGE_CURVE ( 'NONE', #56853, #71627, #60946, .T. ) ;
#17883=CARTESIAN_POINT ( 'NONE',  ( -13.50000000000000178, 0.000000000000000000, 0.000000000000000000 ) ) ;
#17955=CARTESIAN_POINT ( 'NONE',  ( -13.50000000000000000, -7.794228634059976457, -13.00000000000000000 ) ) ;
#18026=ORIENTED_EDGE ( 'NONE', *, *, #50408, .F. ) ;
#18065=ADVANCED_FACE ( 'NONE', ( #13936 ), #31768, .F. ) ;
#18230=EDGE_CURVE ( 'NONE', #38464, #30181, #96998, .T. ) ;
#18331=CARTESIAN_POINT ( 'NONE',  ( 0.000000000000000000, 0.000000000000000000, -13.00000000000000000 ) ) ;
#18482=FACE_OUTER_BOUND ( 'NONE', #50532, .T. ) ;
#18596=DIRECTION ( 'NONE',  ( -0.000000000000000000, -0.000000000000000000, -1.000000000000000000 ) ) ;
#18639=DIRECTION ( 'NONE',  ( -1.000000000000000000, 0.000000000000000000, 0.000000000000000000 ) ) ;
#18653=B_SPLINE_CURVE_WITH_KNOTS ( 'NONE', 3,
 ( #25475, #7114, #83139, #40553, #90710, #16819, #33547, #41090 ),
 .UNSPECIFIED., .F., .F.,
 ( 4, 2, 2, 4 ),
 ( 0.02179091314793462492, 0.02376333058066962614, 0.02573574801340463084, 0.02968058287887463328 ),
 .UNSPECIFIED. ) ;
#18702=UNCERTAINTY_MEASURE_WITH_UNIT (LENGTH_MEASURE( 1.000000000000000082E-05 ), #68023, 'distance_accuracy_value', 'NONE');
#18742=VERTEX_POINT ( 'NONE', #74699 ) ;
#18772=PRESENTATION_STYLE_ASSIGNMENT (( #10101 ) ) ;
#18866=AXIS2_PLACEMENT_3D ( 'NONE', #55127, #29320, #46004 ) ;
#18876=AXIS2_PLACEMENT_3D ( 'NONE', #39977, #31900, #65312 ) ;
#18905=( NAMED_UNIT ( * ) PLANE_ANGLE_UNIT ( ) SI_UNIT ( $, .RADIAN. ) );
#18936=FACE_OUTER_BOUND ( 'NONE', #20170, .T. ) ;
#18988=CIRCLE ( 'NONE', #13770, 8.000000000000000000 ) ;
#18993=EDGE_CURVE ( 'NONE', #88199, #60134, #12652, .T. ) ;
#19061=ORIENTED_EDGE ( 'NONE', *, *, #71525, .F. ) ;
#19074=DIRECTION ( 'NONE',  ( 0.8191520442889974607, 1.003171929053531649E-16, -0.5735764363510380548 ) ) ;
#19147=AXIS2_PLACEMENT_3D ( 'NONE', #89262, #25074, #41228 ) ;
#19168=ORIENTED_EDGE ( 'NONE', *, *, #22963, .T. ) ;
#19232=DIRECTION ( 'NONE',  ( 1.000000000000000000, 0.000000000000000000, 0.000000000000000000 ) ) ;
#19366=ORIENTED_EDGE ( 'NONE', *, *, #77728, .T. ) ;
#19459=CARTESIAN_POINT ( 'NONE',  ( 7.000000000000000000, 0.000000000000000000, -8.125150395352576993 ) ) ;
#19552=ORIENTED_EDGE ( 'NONE', *, *, #65922, .F. ) ;
#19712=CARTESIAN_POINT ( 'NONE',  ( 0.000000000000000000, 0.000000000000000000, -13.00000000000000000 ) ) ;
#19781=FACE_OUTER_BOUND ( 'NONE', #79494, .T. ) ;
#19873=AXIS2_PLACEMENT_3D ( 'NONE', #101376, #21038, #70603 ) ;
#19938=EDGE_CURVE ( 'NONE', #6815, #39498, #87878, .T. ) ;
#19949=FACE_OUTER_BOUND ( 'NONE', #75333, .T. ) ;
#19991=LINE ( 'NONE', #19459, #67437 ) ;
#20015=CARTESIAN_POINT ( 'NONE',  ( 8.000000000000000000, 9.797174393178825657E-16, -1.875285714285714445 ) ) ;
#20032=CARTESIAN_POINT ( 'NONE',  ( -8.000000000000000000, 0.000000000000000000, -12.97459999999999525 ) ) ;
#20170=EDGE_LOOP ( 'NONE', ( #51516, #96686, #92414 ) ) ;
#20215=CARTESIAN_POINT ( 'NONE',  ( 4.463429423125059081, -13.01149508916979336, -12.86120860535740462 ) ) ;
#20275=VECTOR ( 'NONE', #15261, 999.9999999999998863 ) ;
#20395=CARTESIAN_POINT ( 'NONE',  ( 0.000000000000000000, 0.000000000000000000, -0.02540000000000007530 ) ) ;
#20513=VERTEX_POINT ( 'NONE', #14287 ) ;
#20537=DIRECTION ( 'NONE',  ( -0.000000000000000000, -0.000000000000000000, -1.000000000000000000 ) ) ;
#20570=ADVANCED_FACE ( 'NONE', ( #87681 ), #56869, .F. ) ;
#20604=CARTESIAN_POINT ( 'NONE',  ( 13.50000000000000355, -2.625659737069749422, -12.88678781509933380 ) ) ;
#20652=ORIENTED_EDGE ( 'NONE', *, *, #98633, .T. ) ;
#20679=FACE_OUTER_BOUND ( 'NONE', #4672, .T. ) ;
#20808=CARTESIAN_POINT ( 'NONE',  ( 0.000000000000000000, 0.000000000000000000, -1.875285714285714445 ) ) ;
#20885=LINE ( 'NONE', #88221, #79478 ) ;
#20910=CARTESIAN_POINT ( 'NONE',  ( -5.724587470723463412E-14, -15.58845726811991561, -1.205771365940065953 ) ) ;
#20912=AXIS2_PLACEMENT_3D ( 'NONE', #81127, #98893, #15871 ) ;
#20958=CARTESIAN_POINT ( 'NONE',  ( -13.50000000000000178, 0.000000000000000000, 0.000000000000000000 ) ) ;
#20979=AXIS2_PLACEMENT_3D ( 'NONE', #27008, #86296, #51765 ) ;
#20993=LINE ( 'NONE', #5807, #29459 ) ;
#21007=CARTESIAN_POINT ( 'NONE',  ( 4.464296094009049476, 13.01099471650158534, -0.1149164202474796115 ) ) ;
#21038=DIRECTION ( 'NONE',  ( -0.000000000000000000, -0.000000000000000000, -1.000000000000000000 ) ) ;
#21104=ORIENTED_EDGE ( 'NONE', *, *, #94948, .T. ) ;
#21162=CARTESIAN_POINT ( 'NONE',  ( 2.602085213965210642E-15, 15.58845726811991561, -11.79422863405993382 ) ) ;
#21224=VERTEX_POINT ( 'NONE', #106225 ) ;
#21386=CARTESIAN_POINT ( 'NONE',  ( -7.899999792244746466, 11.02739026146940127, 8.477105736121037793E-15 ) ) ;
#21409=CARTESIAN_POINT ( 'NONE',  ( -7.000000000000000000, 8.572527594031471218E-16, -12.27439246179028309 ) ) ;
#21413=FACE_OUTER_BOUND ( 'NONE', #80351, .T. ) ;
#21435=CONICAL_SURFACE ( 'NONE', #57565, 7.000000000000000000, 0.9599310885968753704 ) ;
#21504=VERTEX_POINT ( 'NONE', #24179 ) ;
#21514=VECTOR ( 'NONE', #95791, 999.9999999999998863 ) ;
#21596=ORIENTED_EDGE ( 'NONE', *, *, #43997, .F. ) ;
#21705=ORIENTED_EDGE ( 'NONE', *, *, #69028, .T. ) ;
#21738=AXIS2_PLACEMENT_3D ( 'NONE', #72892, #9226, #73425 ) ;
#21798=CARTESIAN_POINT ( 'NONE',  ( 0.000000000000000000, 0.000000000000000000, -12.97459999999999525 ) ) ;
#21823=DIRECTION ( 'NONE',  ( 0.000000000000000000, 0.000000000000000000, 1.000000000000000000 ) ) ;
#21827=EDGE_LOOP ( 'NONE', ( #5139, #38896, #98374, #59312 ) ) ;
#22026=ORIENTED_EDGE ( 'NONE', *, *, #29366, .F. ) ;
#22101=LINE ( 'NONE', #77670, #63853 ) ;
#22119=ORIENTED_EDGE ( 'NONE', *, *, #26063, .T. ) ;
#22175=CONICAL_SURFACE ( 'NONE', #32562, 8.000000000000000000, 0.9599310885968911355 ) ;
#22266=ORIENTED_EDGE ( 'NONE', *, *, #17686, .T. ) ;
#22269=DIRECTION ( 'NONE',  ( -0.000000000000000000, -0.000000000000000000, -1.000000000000000000 ) ) ;
#22285=EDGE_CURVE ( 'NONE', #42431, #64398, #43491, .T. ) ;
#22328=DIRECTION ( 'NONE',  ( 0.000000000000000000, 0.000000000000000000, -1.000000000000000000 ) ) ;
#22332=DIRECTION ( 'NONE',  ( 0.000000000000000000, 0.000000000000000000, 1.000000000000000000 ) ) ;
#22366=DIRECTION ( 'NONE',  ( -1.000000000000000000, 0.000000000000000000, 0.000000000000000000 ) ) ;
#22470=AXIS2_PLACEMENT_3D ( 'NONE', #92426, #101060, #93520 ) ;
#22493=CARTESIAN_POINT ( 'NONE',  ( 8.000000000000000000, 9.797174393178825657E-16, -9.274828571428571422 ) ) ;
#22582=ORIENTED_EDGE ( 'NONE', *, *, #39934, .T. ) ;
#22955=EDGE_CURVE ( 'NONE', #31665, #44273, #6222, .T. ) ;
#22963=EDGE_CURVE ( 'NONE', #2886, #34061, #102627, .T. ) ;
#22993=ORIENTED_EDGE ( 'NONE', *, *, #75508, .F. ) ;
#23009=CARTESIAN_POINT ( 'NONE',  ( 7.000000000000000000, 0.000000000000000000, -4.425378966781146950 ) ) ;
#23131=ORIENTED_EDGE ( 'NONE', *, *, #8406, .F. ) ;
#23207=EDGE_CURVE ( 'NONE', #18742, #79592, #81968, .T. ) ;
#23224=DIRECTION ( 'NONE',  ( 0.000000000000000000, 0.000000000000000000, 1.000000000000000000 ) ) ;
#23267=VECTOR ( 'NONE', #19074, 1000.000000000000000 ) ;
#23330=CARTESIAN_POINT ( 'NONE',  ( 8.000000000000000000, 9.797174393178825657E-16, -3.725171428571429022 ) ) ;
#23393=ADVANCED_FACE ( 'NONE', ( #39401 ), #105183, .F. ) ;
#23394=VERTEX_POINT ( 'NONE', #56063 ) ;
#23398=LINE ( 'NONE', #48163, #72322 ) ;
#23420=LINE ( 'NONE', #105890, #58232 ) ;
#23469=VECTOR ( 'NONE', #83254, 999.9999999999998863 ) ;
#23528=EDGE_CURVE ( 'NONE', #23394, #95900, #33821, .T. ) ;
#23549=DIRECTION ( 'NONE',  ( -0.000000000000000000, -0.000000000000000000, -1.000000000000000000 ) ) ;
#23661=LINE ( 'NONE', #41405, #48075 ) ;
#23697=DIRECTION ( 'NONE',  ( -1.000000000000000000, 0.000000000000000000, 0.000000000000000000 ) ) ;
#23720=DIRECTION ( 'NONE',  ( 1.000000000000000000, 0.000000000000000000, 0.000000000000000000 ) ) ;
#23727=DIRECTION ( 'NONE',  ( 1.000000000000000000, 0.000000000000000000, 0.000000000000000000 ) ) ;
#23790=CONICAL_SURFACE ( 'NONE', #3123, 13.50000000000000178, 1.047197551196596077 ) ;
#23859=ORIENTED_EDGE ( 'NONE', *, *, #90558, .F. ) ;
#23867=VERTEX_POINT ( 'NONE', #9934 ) ;
#23962=EDGE_CURVE ( 'NONE', #67861, #23867, #48967, .T. ) ;
#24102=ORIENTED_EDGE ( 'NONE', *, *, #36833, .F. ) ;
#24179=CARTESIAN_POINT ( 'NONE',  ( -7.000000000000000000, 8.572527594031471218E-16, -11.82492182392400437 ) ) ;
#24230=ORIENTED_EDGE ( 'NONE', *, *, #63694, .F. ) ;
#24386=DIRECTION ( 'NONE',  ( 0.8191520442889909104, 1.003171929053523637E-16, -0.5735764363510472696 ) ) ;
#24403=CARTESIAN_POINT ( 'NONE',  ( -5.600000207755308601, -12.35529564071044817, -1.068955579434926870E-14 ) ) ;
#24423=DIRECTION ( 'NONE',  ( -0.000000000000000000, -0.000000000000000000, -1.000000000000000000 ) ) ;
#24555=EDGE_LOOP ( 'NONE', ( #42249, #34272, #85856, #29691 ) ) ;
#24559=ADVANCED_FACE ( 'NONE', ( #44608 ), #75275, .F. ) ;
#24594=DIRECTION ( 'NONE',  ( -1.000000000000000000, 0.000000000000000000, 0.000000000000000000 ) ) ;
#24679=EDGE_CURVE ( 'NONE', #16577, #35268, #30961, .T. ) ;
#24719=ORIENTED_EDGE ( 'NONE', *, *, #98287, .T. ) ;
#24728=EDGE_CURVE ( 'NONE', #68006, #104233, #70135, .T. ) ;
#24731=CARTESIAN_POINT ( 'NONE',  ( 0.000000000000000000, 0.000000000000000000, 0.000000000000000000 ) ) ;
#24734=DIRECTION ( 'NONE',  ( -0.000000000000000000, -0.000000000000000000, -1.000000000000000000 ) ) ;
#24773=DIRECTION ( 'NONE',  ( 1.000000000000000000, 0.000000000000000000, 0.000000000000000000 ) ) ;
#24791=EDGE_LOOP ( 'NONE', ( #22119, #66003, #100214, #10379 ) ) ;
#24805=VERTEX_POINT ( 'NONE', #21162 ) ;
#24877=CARTESIAN_POINT ( 'NONE',  ( 0.000000000000000000, 0.000000000000000000, -4.425378966781146950 ) ) ;
#24948=DIRECTION ( 'NONE',  ( -0.000000000000000000, -0.000000000000000000, -1.000000000000000000 ) ) ;
#25016=FACE_OUTER_BOUND ( 'NONE', #38984, .T. ) ;
#25018=ADVANCED_FACE ( 'NONE', ( #67942 ), #42401, .F. ) ;
#25074=DIRECTION ( 'NONE',  ( -0.000000000000000000, -0.000000000000000000, -1.000000000000000000 ) ) ;
#25166=DIRECTION ( 'NONE',  ( 1.000000000000000000, 0.000000000000000000, 0.000000000000000000 ) ) ;
#25167=DIRECTION ( 'NONE',  ( 1.000000000000000000, 0.000000000000000000, 0.000000000000000000 ) ) ;
#25203=ORIENTED_EDGE ( 'NONE', *, *, #101597, .F. ) ;
#25290=CARTESIAN_POINT ( 'NONE',  ( -6.750000000000018652, 11.69134295108991317, 0.000000000000000000 ) ) ;
#25313=DIRECTION ( 'NONE',  ( -0.000000000000000000, -0.000000000000000000, -1.000000000000000000 ) ) ;
#25408=CIRCLE ( 'NONE', #52940, 7.000000000000000000 ) ;
#25414=LINE ( 'NONE', #91199, #7021 ) ;
#25443=VERTEX_POINT ( 'NONE', #71802 ) ;
#25475=CARTESIAN_POINT ( 'NONE',  ( 13.50000000000000178, 0.000000000000000000, -13.00000000000000000 ) ) ;
#25531=DIRECTION ( 'NONE',  ( 0.000000000000000000, 0.000000000000000000, 1.000000000000000000 ) ) ;
#25722=CARTESIAN_POINT ( 'NONE',  ( 0.000000000000000000, 0.000000000000000000, -12.97459999999999525 ) ) ;
#25764=ORIENTED_EDGE ( 'NONE', *, *, #64330, .F. ) ;
#25795=DIRECTION ( 'NONE',  ( -0.8191520442889884679, 1.003171929053520679E-16, 0.5735764363510509334 ) ) ;
#25804=AXIS2_PLACEMENT_3D ( 'NONE', #1862, #58536, #57436 ) ;
#25859=AXIS2_PLACEMENT_3D ( 'NONE', #32362, #81393, #15080 ) ;
#25861=ORIENTED_EDGE ( 'NONE', *, *, #101597, .T. ) ;
#25947=FILL_AREA_STYLE ('',( #99778 ) ) ;
#25997=CARTESIAN_POINT ( 'NONE',  ( 0.000000000000000000, 0.000000000000000000, -13.00000000000000000 ) ) ;
#26063=EDGE_CURVE ( 'NONE', #42431, #15319, #42551, .T. ) ;
#26093=AXIS2_PLACEMENT_3D ( 'NONE', #70970, #105459, #96328 ) ;
#26097=ORIENTED_EDGE ( 'NONE', *, *, #50408, .T. ) ;
#26234=AXIS2_PLACEMENT_3D ( 'NONE', #91302, #25531, #43792 ) ;
#26313=ADVANCED_FACE ( 'NONE', ( #87230 ), #13312, .F. ) ;
#26325=CARTESIAN_POINT ( 'NONE',  ( 11.28351131189991641, -9.073918974790325720, -12.46553453015538793 ) ) ;
#26342=SURFACE_STYLE_FILL_AREA ( #92080 ) ;
#26357=FACE_OUTER_BOUND ( 'NONE', #15133, .T. ) ;
#26371=EDGE_CURVE ( 'NONE', #71961, #44907, #97748, .T. ) ;
#26455=EDGE_LOOP ( 'NONE', ( #35125, #38183, #72142, #74344 ) ) ;
#26466=SURFACE_STYLE_FILL_AREA ( #25947 ) ;
#26535=VERTEX_POINT ( 'NONE', #104879 ) ;
#26597=CARTESIAN_POINT ( 'NONE',  ( 0.000000000000000000, 0.000000000000000000, -9.975036109638290682 ) ) ;
#26600=ORIENTED_EDGE ( 'NONE', *, *, #3275, .T. ) ;
#26715=ORIENTED_EDGE ( 'NONE', *, *, #42462, .F. ) ;
#26791=ORIENTED_EDGE ( 'NONE', *, *, #46196, .F. ) ;
#26855=ADVANCED_FACE ( 'NONE', ( #58724 ), #17206, .F. ) ;
#26920=DIRECTION ( 'NONE',  ( -1.000000000000000000, 0.000000000000000000, 0.000000000000000000 ) ) ;
#26961=DIRECTION ( 'NONE',  ( 0.000000000000000000, 0.000000000000000000, 1.000000000000000000 ) ) ;
#27008=CARTESIAN_POINT ( 'NONE',  ( 0.000000000000000000, 0.000000000000000000, -9.975036109638290682 ) ) ;
#27035=ORIENTED_EDGE ( 'NONE', *, *, #80092, .F. ) ;
#27086=EDGE_LOOP ( 'NONE', ( #47654, #60528, #65878, #27892 ) ) ;
#27126=CARTESIAN_POINT ( 'NONE',  ( -8.000000000000000000, 9.797174393178825657E-16, -25.03750572909317285 ) ) ;
#27166=EDGE_CURVE ( 'NONE', #3430, #21504, #13433, .T. ) ;
#27185=EDGE_CURVE ( 'NONE', #95900, #23394, #80572, .T. ) ;
#27248=CIRCLE ( 'NONE', #77162, 13.50000000000000000 ) ;
#27358=DIRECTION ( 'NONE',  ( -0.000000000000000000, -0.000000000000000000, -1.000000000000000000 ) ) ;
#27426=CIRCLE ( 'NONE', #18876, 7.981862520314372489 ) ;
#27455=DIRECTION ( 'NONE',  ( -0.000000000000000000, -0.000000000000000000, -1.000000000000000000 ) ) ;
#27564=CARTESIAN_POINT ( 'NONE',  ( 0.000000000000000000, 0.000000000000000000, -13.00000000000000000 ) ) ;
#27619=CARTESIAN_POINT ( 'NONE',  ( 11.28790243858420084, 9.071383756617068528, -0.5355294694855753379 ) ) ;
#27632=CIRCLE ( 'NONE', #87870, 7.000000000000000000 ) ;
#27670=AXIS2_PLACEMENT_3D ( 'NONE', #36170, #20537, #93304 ) ;
#27698=LINE ( 'NONE', #99936, #23267 ) ;
#27703=EDGE_LOOP ( 'NONE', ( #58717, #22026, #85919 ) ) ;
#27774=CARTESIAN_POINT ( 'NONE',  ( 5.601730134768060587, -12.35429686688395989, -12.97150009825808148 ) ) ;
#27785=ORIENTED_EDGE ( 'NONE', *, *, #90377, .F. ) ;
#27819=EDGE_LOOP ( 'NONE', ( #49477, #99642, #105559, #7349 ) ) ;
#27823=DIRECTION ( 'NONE',  ( 0.000000000000000000, 0.000000000000000000, 1.000000000000000000 ) ) ;
#27856=CARTESIAN_POINT ( 'NONE',  ( 0.000000000000000000, 0.000000000000000000, -1.875285714285714445 ) ) ;
#27892=ORIENTED_EDGE ( 'NONE', *, *, #61995, .T. ) ;
#27977=CARTESIAN_POINT ( 'NONE',  ( -13.49999999999999822, 2.646256834279067771, -0.1392913482116606150 ) ) ;
#28061=SHAPE_REPRESENTATION_RELATIONSHIP ( 'NONE' , 'NONE' ,  #74292, #67921 ) ;
#28087=FACE_OUTER_BOUND ( 'NONE', #46013, .T. ) ;
#28148=CARTESIAN_POINT ( 'NONE',  ( 0.000000000000000000, 0.000000000000000000, -13.00000000000000000 ) ) ;
#28182=CIRCLE ( 'NONE', #88426, 7.000000000000000000 ) ;
#28458=CONICAL_SURFACE ( 'NONE', #83528, 13.50000000000000178, 1.047197551196596077 ) ;
#28493=CARTESIAN_POINT ( 'NONE',  ( -13.49999999999999822, 0.6589394956329776010, 1.021521734388685814E-15 ) ) ;
#28540=B_SPLINE_CURVE_WITH_KNOTS ( 'NONE', 3,
 ( #28941, #53689, #4619, #60221, #93089, #62333 ),
 .UNSPECIFIED., .F., .F.,
 ( 4, 2, 4 ),
 ( 2.380729204624338438E-07, 0.003943479449179648072, 0.007886720825438833446 ),
 .UNSPECIFIED. ) ;
#28681=DIRECTION ( 'NONE',  ( -1.000000000000000000, -8.881784197001252323E-16, 0.000000000000000000 ) ) ;
#28740=CARTESIAN_POINT ( 'NONE',  ( 2.235495008889195345E-15, -15.58845726811994759, -13.00000000000000000 ) ) ;
#28760=VECTOR ( 'NONE', #29299, 999.9999999999998863 ) ;
#28872=CARTESIAN_POINT ( 'NONE',  ( -7.000000000000000000, 8.572527594031471218E-16, -9.975036109638290682 ) ) ;
#28941=CARTESIAN_POINT ( 'NONE',  ( 2.602085213965210642E-15, 15.58845726811991561, -11.79422863405993382 ) ) ;
#29012=ORIENTED_EDGE ( 'NONE', *, *, #97494, .T. ) ;
#29054=ORIENTED_EDGE ( 'NONE', *, *, #31655, .T. ) ;
#29055=EDGE_LOOP ( 'NONE', ( #101048, #44579, #91610, #98305 ) ) ;
#29113=DIRECTION ( 'NONE',  ( 1.000000000000000000, 0.000000000000000000, 0.000000000000000000 ) ) ;
#29247=ORIENTED_EDGE ( 'NONE', *, *, #14700, .F. ) ;
#29269=EDGE_CURVE ( 'NONE', #99841, #16577, #16648, .T. ) ;
#29299=DIRECTION ( 'NONE',  ( 0.8191520442889884679, 0.000000000000000000, 0.5735764363510509334 ) ) ;
#29320=DIRECTION ( 'NONE',  ( -0.000000000000000000, -0.000000000000000000, 1.000000000000000000 ) ) ;
#29361=AXIS2_PLACEMENT_3D ( 'NONE', #93566, #21823, #87596 ) ;
#29366=EDGE_CURVE ( 'NONE', #33682, #104233, #54661, .T. ) ;
#29391=PRODUCT_CONTEXT ( 'NONE', #12143, 'mechanical' ) ;
#29459=VECTOR ( 'NONE', #55408, 1000.000000000000000 ) ;
#29489=DIRECTION ( 'NONE',  ( 0.000000000000000000, 0.000000000000000000, 1.000000000000000000 ) ) ;
#29534=CARTESIAN_POINT ( 'NONE',  ( -7.000000000000000000, 8.572527594031471218E-16, -4.425378966781146950 ) ) ;
#29665=EDGE_CURVE ( 'NONE', #44183, #26535, #48492, .T. ) ;
#29676=ORIENTED_EDGE ( 'NONE', *, *, #4195, .F. ) ;
#29681=LINE ( 'NONE', #78707, #82455 ) ;
#29691=ORIENTED_EDGE ( 'NONE', *, *, #4531, .T. ) ;
#29754=EDGE_LOOP ( 'NONE', ( #46018, #84585, #39393 ) ) ;
#29955=CARTESIAN_POINT ( 'NONE',  ( -1.104211576045348808, -14.95094041744786040, -12.16229915940863116 ) ) ;
#30085=EDGE_LOOP ( 'NONE', ( #31573, #250, #16311, #54199 ) ) ;
#30115=ORIENTED_EDGE ( 'NONE', *, *, #3275, .F. ) ;
#30181=VERTEX_POINT ( 'NONE', #30379 ) ;
#30251=DIRECTION ( 'NONE',  ( 1.000000000000000000, 0.000000000000000000, 0.000000000000000000 ) ) ;
#30253=CARTESIAN_POINT ( 'NONE',  ( 0.000000000000000000, 0.000000000000000000, -13.00000000000000000 ) ) ;
#30289=DIRECTION ( 'NONE',  ( -0.000000000000000000, -0.000000000000000000, -1.000000000000000000 ) ) ;
#30312=EDGE_LOOP ( 'NONE', ( #23859, #20652, #47213, #102827 ) ) ;
#30324=EDGE_CURVE ( 'NONE', #25443, #91936, #75313, .T. ) ;
#30379=CARTESIAN_POINT ( 'NONE',  ( -8.000000000000000000, 0.000000000000000000, -0.02540000000000007530 ) ) ;
#30452=LINE ( 'NONE', #5616, #38004 ) ;
#30586=VECTOR ( 'NONE', #48098, 999.9999999999998863 ) ;
#30588=ADVANCED_FACE ( 'NONE', ( #58210 ), #97872, .F. ) ;
#30636=VERTEX_POINT ( 'NONE', #101861 ) ;
#30657=AXIS2_PLACEMENT_3D ( 'NONE', #25722, #76334, #19232 ) ;
#30717=CARTESIAN_POINT ( 'NONE',  ( -6.750000000000018652, 11.69134295108991317, -13.00000000000000000 ) ) ;
#30919=ADVANCED_FACE ( 'NONE', ( #37706 ), #5304, .F. ) ;
#30926=DIRECTION ( 'NONE',  ( -0.000000000000000000, 0.000000000000000000, -1.000000000000000000 ) ) ;
#30938=ORIENTED_EDGE ( 'NONE', *, *, #4796, .T. ) ;
#30961=LINE ( 'NONE', #41143, #106284 ) ;
#31146=CARTESIAN_POINT ( 'NONE',  ( 0.000000000000000000, 0.000000000000000000, -0.02540000000000007530 ) ) ;
#31150=DIRECTION ( 'NONE',  ( 0.000000000000000000, -0.000000000000000000, 1.000000000000000000 ) ) ;
#31238=CIRCLE ( 'NONE', #26093, 7.000000000000000000 ) ;
#31243=FACE_OUTER_BOUND ( 'NONE', #43015, .T. ) ;
#31341=EDGE_CURVE ( 'NONE', #6815, #88199, #53156, .T. ) ;
#31388=EDGE_LOOP ( 'NONE', ( #102873, #86124, #22582, #12198, #13554, #94552 ) ) ;
#31427=CIRCLE ( 'NONE', #95159, 7.000000000000000000 ) ;
#31454=DIRECTION ( 'NONE',  ( -0.000000000000000000, -0.000000000000000000, -1.000000000000000000 ) ) ;
#31485=CYLINDRICAL_SURFACE ( 'NONE', #98811, 7.000000000000000000 ) ;
#31573=ORIENTED_EDGE ( 'NONE', *, *, #106064, .F. ) ;
#31586=DIRECTION ( 'NONE',  ( 0.000000000000000000, 0.000000000000000000, 1.000000000000000000 ) ) ;
#31648=ORIENTED_EDGE ( 'NONE', *, *, #57813, .F. ) ;
#31655=EDGE_CURVE ( 'NONE', #44183, #88199, #71100, .T. ) ;
#31665=VERTEX_POINT ( 'NONE', #85536 ) ;
#31671=CARTESIAN_POINT ( 'NONE',  ( 0.000000000000000000, 0.000000000000000000, -13.00000000000000000 ) ) ;
#31677=CARTESIAN_POINT ( 'NONE',  ( -8.000000000000000000, 0.000000000000000000, -0.02540000000000007530 ) ) ;
#31768=CONICAL_SURFACE ( 'NONE', #73072, 8.000000000000000000, 0.9599310885968911355 ) ;
#31900=DIRECTION ( 'NONE',  ( 0.000000000000000000, 0.000000000000000000, 1.000000000000000000 ) ) ;
#32034=CARTESIAN_POINT ( 'NONE',  ( 0.000000000000000000, 0.000000000000000000, 3.469446951953614189E-15 ) ) ;
#32099=ORIENTED_EDGE ( 'NONE', *, *, #10849, .T. ) ;
#32107=EDGE_CURVE ( 'NONE', #58987, #96238, #106708, .T. ) ;
#32238=CARTESIAN_POINT ( 'NONE',  ( -13.50000000000000000, 7.794228634059933825, -13.00000000000000000 ) ) ;
#32362=CARTESIAN_POINT ( 'NONE',  ( 0.000000000000000000, 0.000000000000000000, -1.175078176076019387 ) ) ;
#32470=CARTESIAN_POINT ( 'NONE',  ( 8.000000000000000000, 9.797174393178825657E-16, -12.97459999999999525 ) ) ;
#32562=AXIS2_PLACEMENT_3D ( 'NONE', #47653, #80020, #22366 ) ;
#32645=EDGE_CURVE ( 'NONE', #34061, #2886, #61790, .T. ) ;
#32769=DIRECTION ( 'NONE',  ( -1.000000000000000000, 0.000000000000000000, 0.000000000000000000 ) ) ;
#32816=ADVANCED_FACE ( 'NONE', ( #1416 ), #53376, .F. ) ;
#32837=CARTESIAN_POINT ( 'NONE',  ( 7.000000000000000000, 0.000000000000000000, -13.00000000000000000 ) ) ;
#32846=VERTEX_POINT ( 'NONE', #67253 ) ;
#32858=DIRECTION ( 'NONE',  ( -0.000000000000000000, -0.000000000000000000, -1.000000000000000000 ) ) ;
#32866=ORIENTED_EDGE ( 'NONE', *, *, #71525, .T. ) ;
#32906=VERTEX_POINT ( 'NONE', #49447 ) ;
#32942=ORIENTED_EDGE ( 'NONE', *, *, #45393, .T. ) ;
#32950=AXIS2_PLACEMENT_3D ( 'NONE', #74732, #97410, #25166 ) ;
#33015=CARTESIAN_POINT ( 'NONE',  ( -13.50000000000000000, -2.625659737069750754, -0.1132121849006608727 ) ) ;
#33254=ORIENTED_EDGE ( 'NONE', *, *, #17686, .F. ) ;
#33275=DIRECTION ( 'NONE',  ( -1.000000000000000000, 0.000000000000000000, 0.000000000000000000 ) ) ;
#33290=ORIENTED_EDGE ( 'NONE', *, *, #32645, .T. ) ;
#33333=DIRECTION ( 'NONE',  ( -0.000000000000000000, -0.000000000000000000, 1.000000000000000000 ) ) ;
#33365=VERTEX_POINT ( 'NONE', #76125 ) ;
#33369=LINE ( 'NONE', #9056, #48433 ) ;
#33373=DIRECTION ( 'NONE',  ( 0.000000000000000000, 0.000000000000000000, 1.000000000000000000 ) ) ;
#33466=CARTESIAN_POINT ( 'NONE',  ( 13.50000000000000355, 7.794228634059978233, -11.79422863405993382 ) ) ;
#33547=CARTESIAN_POINT ( 'NONE',  ( 13.50000000000000711, 6.533945317241104611, -12.15804109017022583 ) ) ;
#33682=VERTEX_POINT ( 'NONE', #51716 ) ;
#33716=ORIENTED_EDGE ( 'NONE', *, *, #42069, .F. ) ;
#33724=B_SPLINE_CURVE_WITH_KNOTS ( 'NONE', 3,
 ( #55032, #63697, #62114, #72292, #53971, #97097 ),
 .UNSPECIFIED., .F., .F.,
 ( 4, 2, 4 ),
 ( 0.01390592816464532311, 0.01784842065628997054, 0.02179091314793462145 ),
 .UNSPECIFIED. ) ;
#33821=CIRCLE ( 'NONE', #49334, 8.000000000000000000 ) ;
#33904=AXIS2_PLACEMENT_3D ( 'NONE', #51313, #38746, #95915 ) ;
#33932=CIRCLE ( 'NONE', #94206, 7.000000000000000000 ) ;
#33969=ORIENTED_EDGE ( 'NONE', *, *, #1262, .T. ) ;
#34007=ORIENTED_EDGE ( 'NONE', *, *, #23207, .T. ) ;
#34061=VERTEX_POINT ( 'NONE', #92093 ) ;
#34068=CARTESIAN_POINT ( 'NONE',  ( 0.000000000000000000, 0.000000000000000000, 0.000000000000000000 ) ) ;
#34135=CARTESIAN_POINT ( 'NONE',  ( -7.000000000000000000, 8.572527594031471218E-16, -2.575493252495433261 ) ) ;
#34236=DIRECTION ( 'NONE',  ( 0.8191520442889911324, 0.000000000000000000, 0.5735764363510470476 ) ) ;
#34261=ORIENTED_EDGE ( 'NONE', *, *, #18993, .T. ) ;
#34272=ORIENTED_EDGE ( 'NONE', *, *, #98633, .F. ) ;
#34348=VERTEX_POINT ( 'NONE', #29534 ) ;
#34380=DIRECTION ( 'NONE',  ( -1.000000000000000000, 0.000000000000000000, 0.000000000000000000 ) ) ;
#34385=ORIENTED_EDGE ( 'NONE', *, *, #104139, .T. ) ;
#34410=CONICAL_SURFACE ( 'NONE', #25804, 7.000000000000000000, 0.9599310885968753704 ) ;
#34451=LINE ( 'NONE', #32837, #86584 ) ;
#34478=CARTESIAN_POINT ( 'NONE',  ( -13.50000000000000355, 5.257130651325599757, -12.46102409077683326 ) ) ;
#34504=FACE_OUTER_BOUND ( 'NONE', #29754, .T. ) ;
#34505=CARTESIAN_POINT ( 'NONE',  ( -9.601913782316103152, -10.04478976116414835, -12.77952306666688287 ) ) ;
#34548=DIRECTION ( 'NONE',  ( -0.000000000000000000, -0.000000000000000000, -1.000000000000000000 ) ) ;
#34598=EDGE_CURVE ( 'NONE', #14406, #52643, #91456, .T. ) ;
#34647=CYLINDRICAL_SURFACE ( 'NONE', #9037, 7.000000000000000000 ) ;
#34749=LINE ( 'NONE', #90831, #23469 ) ;
#34766=EDGE_CURVE ( 'NONE', #24805, #84222, #30452, .T. ) ;
#34777=CONICAL_SURFACE ( 'NONE', #58846, 7.000000000000000000, 0.9599310885968753704 ) ;
#34898=CARTESIAN_POINT ( 'NONE',  ( -8.000000000000000000, 0.000000000000000000, -12.97459999999999525 ) ) ;
#35072=DIRECTION ( 'NONE',  ( 0.000000000000000000, 0.000000000000000000, -1.000000000000000000 ) ) ;
#35125=ORIENTED_EDGE ( 'NONE', *, *, #44908, .F. ) ;
#35154=CARTESIAN_POINT ( 'NONE',  ( 13.50000000000000178, 0.000000000000000000, -13.00000000000000000 ) ) ;
#35175=CARTESIAN_POINT ( 'NONE',  ( -8.673617379884035472E-16, 15.58845726811991561, -1.205771365940065953 ) ) ;
#35268=VERTEX_POINT ( 'NONE', #85507 ) ;
#35338=CARTESIAN_POINT ( 'NONE',  ( 0.000000000000000000, 0.000000000000000000, -4.425378966781146950 ) ) ;
#35382=CONICAL_SURFACE ( 'NONE', #95646, 6.900000000000000355, 0.9599310885968801443 ) ;
#35504=ORIENTED_EDGE ( 'NONE', *, *, #38069, .T. ) ;
#35517=B_SPLINE_CURVE_WITH_KNOTS ( 'NONE', 3,
 ( #25290, #58699, #9583, #73794, #81344, #56537, #89468, #41435 ),
 .UNSPECIFIED., .F., .F.,
 ( 4, 2, 2, 4 ),
 ( 0.007886720825438788343, 0.009850969036564002912, 0.01181521724768921748, 0.01574371366993964488 ),
 .UNSPECIFIED. ) ;
#35522=AXIS2_PLACEMENT_3D ( 'NONE', #59433, #24948, #92296 ) ;
#35551=CARTESIAN_POINT ( 'NONE',  ( 7.000000000000000000, 0.000000000000000000, -2.575493252495433261 ) ) ;
#35569=ORIENTED_EDGE ( 'NONE', *, *, #57813, .T. ) ;
#35786=DIRECTION ( 'NONE',  ( -0.000000000000000000, -0.000000000000000000, -1.000000000000000000 ) ) ;
#35850=EDGE_CURVE ( 'NONE', #105782, #74189, #64799, .T. ) ;
#35947=AXIS2_PLACEMENT_3D ( 'NONE', #86770, #71087, #70571 ) ;
#35976=FACE_OUTER_BOUND ( 'NONE', #29055, .T. ) ;
#36170=CARTESIAN_POINT ( 'NONE',  ( 0.000000000000000000, 0.000000000000000000, -4.874849604647447876 ) ) ;
#36295=CARTESIAN_POINT ( 'NONE',  ( 6.750000000000016875, -11.69134295108991495, -13.00000000000000000 ) ) ;
#36328=ORIENTED_EDGE ( 'NONE', *, *, #92109, .F. ) ;
#36346=ORIENTED_EDGE ( 'NONE', *, *, #94451, .T. ) ;
#36375=EDGE_CURVE ( 'NONE', #3555, #32846, #68219, .T. ) ;
#36428=DIRECTION ( 'NONE',  ( 1.000000000000000000, 0.000000000000000000, 0.000000000000000000 ) ) ;
#36545=CARTESIAN_POINT ( 'NONE',  ( 0.000000000000000000, 0.000000000000000000, -6.275264681066861527 ) ) ;
#36816=CARTESIAN_POINT ( 'NONE',  ( 7.000000000000000000, 0.000000000000000000, -3.024963890361733743 ) ) ;
#36833=EDGE_CURVE ( 'NONE', #3430, #95900, #6027, .T. ) ;
#36906=CARTESIAN_POINT ( 'NONE',  ( -7.000000000000000000, 8.572527594031471218E-16, -1.175078176076019387 ) ) ;
#36936=ORIENTED_EDGE ( 'NONE', *, *, #77728, .F. ) ;
#37036=CIRCLE ( 'NONE', #19873, 7.000000000000000000 ) ;
#37124=AXIS2_PLACEMENT_3D ( 'NONE', #106408, #65439, #91839 ) ;
#37153=CIRCLE ( 'NONE', #73271, 8.000000000000000000 ) ;
#37172=PLANE ( 'NONE',  #98302 ) ;
#37269=ORIENTED_EDGE ( 'NONE', *, *, #92857, .T. ) ;
#37275=ADVANCED_FACE ( 'NONE', ( #87909 ), #1188, .T. ) ;
#37282=CARTESIAN_POINT ( 'NONE',  ( -6.750000000000015099, -11.69134295108991495, -13.00000000000000000 ) ) ;
#37479=CONICAL_SURFACE ( 'NONE', #39219, 7.000000000000000000, 0.9599310885968753704 ) ;
#37512=ORIENTED_EDGE ( 'NONE', *, *, #66692, .T. ) ;
#37658=CARTESIAN_POINT ( 'NONE',  ( -13.50000000000000000, 5.257130651325558013, -0.5389759092231611870 ) ) ;
#37706=FACE_OUTER_BOUND ( 'NONE', #3002, .T. ) ;
#37756=CARTESIAN_POINT ( 'NONE',  ( 2.602085213965210642E-15, 15.58845726811991561, -11.79422863405993382 ) ) ;
#37812=VECTOR ( 'NONE', #86956, 1000.000000000000000 ) ;
#37861=AXIS2_PLACEMENT_3D ( 'NONE', #92410, #84866, #10948 ) ;
#37981=CARTESIAN_POINT ( 'NONE',  ( 6.177150199754222193, -12.02207793746709008, -12.99999999999998757 ) ) ;
#37993=ORIENTED_EDGE ( 'NONE', *, *, #92857, .F. ) ;
#38004=VECTOR ( 'NONE', #80552, 1000.000000000000000 ) ;
#38069=EDGE_CURVE ( 'NONE', #33365, #39498, #18653, .T. ) ;
#38107=CARTESIAN_POINT ( 'NONE',  ( -9.035703905990970952, 10.37169118567824810, -0.1149164202474761975 ) ) ;
#38114=EDGE_CURVE ( 'NONE', #56403, #100438, #49158, .T. ) ;
#38115=ORIENTED_EDGE ( 'NONE', *, *, #24728, .F. ) ;
#38183=ORIENTED_EDGE ( 'NONE', *, *, #29269, .F. ) ;
#38184=EDGE_CURVE ( 'NONE', #64513, #71627, #66970, .T. ) ;
#38296=CARTESIAN_POINT ( 'NONE',  ( 8.000000000000000000, 9.797174393178825657E-16, -12.97459999999999525 ) ) ;
#38325=ORIENTED_EDGE ( 'NONE', *, *, #43829, .T. ) ;
#38349=ADVANCED_FACE ( 'NONE', ( #40175 ), #48779, .F. ) ;
#38403=CARTESIAN_POINT ( 'NONE',  ( 0.000000000000000000, 0.000000000000000000, -0.7256075382097185722 ) ) ;
#38464=VERTEX_POINT ( 'NONE', #75182 ) ;
#38523=FACE_OUTER_BOUND ( 'NONE', #96393, .T. ) ;
#38571=CARTESIAN_POINT ( 'NONE',  ( -5.600000207755311266, -12.35529564071044994, -12.99999999999999112 ) ) ;
#38654=ORIENTED_EDGE ( 'NONE', *, *, #29665, .F. ) ;
#38724=ORIENTED_EDGE ( 'NONE', *, *, #80375, .T. ) ;
#38746=DIRECTION ( 'NONE',  ( -0.000000000000000000, 0.000000000000000000, -1.000000000000000000 ) ) ;
#38831=DIRECTION ( 'NONE',  ( -1.000000000000000000, 0.000000000000000000, 0.000000000000000000 ) ) ;
#38866=CARTESIAN_POINT ( 'NONE',  ( 13.50000000000000355, -5.228219631169429782, -0.5328967677612925780 ) ) ;
#38896=ORIENTED_EDGE ( 'NONE', *, *, #87921, .T. ) ;
#38966=CARTESIAN_POINT ( 'NONE',  ( 0.000000000000000000, 0.000000000000000000, -10.42450674750459072 ) ) ;
#38984=EDGE_LOOP ( 'NONE', ( #71611, #11384, #42410, #35504, #17617, #65438 ) ) ;
#39171=CONICAL_SURFACE ( 'NONE', #16831, 13.50000000000000178, 1.047197551196596077 ) ;
#39219=AXIS2_PLACEMENT_3D ( 'NONE', #105448, #31586, #64473 ) ;
#39294=CIRCLE ( 'NONE', #66840, 8.000000000000000000 ) ;
#39355=ORIENTED_EDGE ( 'NONE', *, *, #42069, .T. ) ;
#39392=ORIENTED_EDGE ( 'NONE', *, *, #30324, .T. ) ;
#39393=ORIENTED_EDGE ( 'NONE', *, *, #82149, .T. ) ;
#39401=FACE_OUTER_BOUND ( 'NONE', #30312, .T. ) ;
#39402=CARTESIAN_POINT ( 'NONE',  ( 13.50000000000000178, 0.000000000000000000, 0.000000000000000000 ) ) ;
#39425=AXIS2_PLACEMENT_3D ( 'NONE', #41991, #25313, #82988 ) ;
#39498=VERTEX_POINT ( 'NONE', #33466 ) ;
#39508=CARTESIAN_POINT ( 'NONE',  ( 4.463429423125061746, -13.01149508916979336, -0.1387913946425961276 ) ) ;
#39596=AXIS2_PLACEMENT_3D ( 'NONE', #89502, #8567, #23727 ) ;
#39780=ADVANCED_FACE ( 'NONE', ( #21413 ), #15304, .T. ) ;
#39836=DIRECTION ( 'NONE',  ( -0.8191520442889884679, 1.003171929053520679E-16, 0.5735764363510509334 ) ) ;
#39891=CARTESIAN_POINT ( 'NONE',  ( 0.000000000000000000, 0.000000000000000000, -0.7702282920306786629 ) ) ;
#39934=EDGE_CURVE ( 'NONE', #68006, #33682, #60659, .T. ) ;
#39977=CARTESIAN_POINT ( 'NONE',  ( 0.000000000000000000, 0.000000000000000000, -0.01269999999999830292 ) ) ;
#40175=FACE_OUTER_BOUND ( 'NONE', #95262, .T. ) ;
#40178=ORIENTED_EDGE ( 'NONE', *, *, #90377, .T. ) ;
#40255=DIRECTION ( 'NONE',  ( 0.000000000000000000, 0.000000000000000000, 1.000000000000000000 ) ) ;
#40261=VECTOR ( 'NONE', #63208, 1000.000000000000000 ) ;
#40359=CARTESIAN_POINT ( 'NONE',  ( -7.898269865231991815, -11.02838903529593928, -0.02849990174191728218 ) ) ;
#40396=CIRCLE ( 'NONE', #7665, 8.000000000000000000 ) ;
#40507=DIRECTION ( 'NONE',  ( -1.000000000000000000, 0.000000000000000000, 0.000000000000000000 ) ) ;
#40520=ORIENTED_EDGE ( 'NONE', *, *, #56251, .F. ) ;
#40553=CARTESIAN_POINT ( 'NONE',  ( 13.50000000000000355, 2.646256834279079317, -12.86070865178833600 ) ) ;
#40611=ADVANCED_FACE ( 'NONE', ( #102467 ), #101406, .F. ) ;
#40630=DIRECTION ( 'NONE',  ( -0.8191520442889884679, 1.003171929053520679E-16, 0.5735764363510509334 ) ) ;
#40947=AXIS2_PLACEMENT_3D ( 'NONE', #41450, #32858, #66258 ) ;
#40966=CIRCLE ( 'NONE', #90942, 7.000000000000000000 ) ;
#41016=( NAMED_UNIT ( * ) PLANE_ANGLE_UNIT ( ) SI_UNIT ( $, .RADIAN. ) );
#41017=AXIS2_PLACEMENT_3D ( 'NONE', #58171, #82987, #24773 ) ;
#41041=CARTESIAN_POINT ( 'NONE',  ( 0.000000000000000000, 0.000000000000000000, 0.000000000000000000 ) ) ;
#41090=CARTESIAN_POINT ( 'NONE',  ( 13.50000000000000355, 7.794228634059978233, -11.79422863405993382 ) ) ;
#41143=CARTESIAN_POINT ( 'NONE',  ( 7.000000000000000000, 0.000000000000000000, -13.00000000000000000 ) ) ;
#41178=PLANE ( 'NONE',  #64973 ) ;
#41228=DIRECTION ( 'NONE',  ( -1.000000000000000000, 0.000000000000000000, 0.000000000000000000 ) ) ;
#41405=CARTESIAN_POINT ( 'NONE',  ( -7.000000000000000000, 8.572527594031471218E-16, -13.00000000000000000 ) ) ;
#41429=ORIENTED_EDGE ( 'NONE', *, *, #97494, .F. ) ;
#41435=CARTESIAN_POINT ( 'NONE',  ( -8.673617379884035472E-16, 15.58845726811991561, -1.205771365940065953 ) ) ;
#41438=CONICAL_SURFACE ( 'NONE', #84574, 8.000000000000000000, 0.9599310885968911355 ) ;
#41450=CARTESIAN_POINT ( 'NONE',  ( 0.000000000000000000, 0.000000000000000000, -2.575493252495433261 ) ) ;
#41470=EDGE_CURVE ( 'NONE', #30636, #50065, #49713, .T. ) ;
#41474=EDGE_LOOP ( 'NONE', ( #3029, #19061, #94879, #22266 ) ) ;
#41482=DIRECTION ( 'NONE',  ( -0.000000000000000000, -0.000000000000000000, 1.000000000000000000 ) ) ;
#41513=ORIENTED_EDGE ( 'NONE', *, *, #57369, .F. ) ;
#41586=LINE ( 'NONE', #91226, #78377 ) ;
#41610=CARTESIAN_POINT ( 'NONE',  ( -13.50000000000000178, -5.228219631169439552, -0.5328967677612923559 ) ) ;
#41613=ORIENTED_EDGE ( 'NONE', *, *, #42155, .F. ) ;
#41754=DIRECTION ( 'NONE',  ( 1.000000000000000000, 0.000000000000000000, 0.000000000000000000 ) ) ;
#41774=DIRECTION ( 'NONE',  ( -1.000000000000000000, 0.000000000000000000, 0.000000000000000000 ) ) ;
#41960=CARTESIAN_POINT ( 'NONE',  ( 0.000000000000000000, 0.000000000000000000, -3.725171428571429022 ) ) ;
#41991=CARTESIAN_POINT ( 'NONE',  ( 0.000000000000000000, 0.000000000000000000, -7.424942857142857733 ) ) ;
#42069=EDGE_CURVE ( 'NONE', #67861, #33365, #27248, .T. ) ;
#42108=CARTESIAN_POINT ( 'NONE',  ( 7.000000000000000000, 0.000000000000000000, -2.575493252495433261 ) ) ;
#42155=EDGE_CURVE ( 'NONE', #60873, #50065, #2339, .T. ) ;
#42249=ORIENTED_EDGE ( 'NONE', *, *, #35850, .F. ) ;
#42267=CARTESIAN_POINT ( 'NONE',  ( 12.39854599882998976, 8.430153398135438181, -12.16137996778342334 ) ) ;
#42340=CARTESIAN_POINT ( 'NONE',  ( -7.981862520314372489, 9.786068389958022714E-16, -0.01269999999999830292 ) ) ;
#42401=CONICAL_SURFACE ( 'NONE', #54466, 8.000000000000000000, 0.9599310885968911355 ) ;
#42410=ORIENTED_EDGE ( 'NONE', *, *, #42462, .T. ) ;
#42413=CIRCLE ( 'NONE', #21738, 8.000000000000000000 ) ;
#42430=EDGE_LOOP ( 'NONE', ( #23131, #34007, #32099, #43318 ) ) ;
#42431=VERTEX_POINT ( 'NONE', #101459 ) ;
#42451=CARTESIAN_POINT ( 'NONE',  ( 6.750000000000016875, -11.69134295108991495, -13.00000000000000000 ) ) ;
#42462=EDGE_CURVE ( 'NONE', #56403, #33365, #92500, .T. ) ;
#42465=FILL_AREA_STYLE_COLOUR ( '', #65275 ) ;
#42482=CARTESIAN_POINT ( 'NONE',  ( 0.000000000000000000, 0.000000000000000000, -0.02540000000000007530 ) ) ;
#42483=CARTESIAN_POINT ( 'NONE',  ( -13.50000000000000000, -7.794228634059985339, -1.205771365940065953 ) ) ;
#42551=CIRCLE ( 'NONE', #106279, 7.000000000000000000 ) ;
#42557=ORIENTED_EDGE ( 'NONE', *, *, #85211, .F. ) ;
#42672=CARTESIAN_POINT ( 'NONE',  ( -1.104211576045346144, -14.95094041744786750, -0.8377008405913687339 ) ) ;
#42807=CARTESIAN_POINT ( 'NONE',  ( 11.28790243858419906, 9.071383756617064975, -12.46447053051442744 ) ) ;
#42840=CARTESIAN_POINT ( 'NONE',  ( 0.000000000000000000, 0.000000000000000000, -7.424942857142857733 ) ) ;
#42858=AXIS2_PLACEMENT_3D ( 'NONE', #32034, #17437, #105375 ) ;
#42929=DIRECTION ( 'NONE',  ( 0.000000000000000000, 0.000000000000000000, 1.000000000000000000 ) ) ;
#42980=CARTESIAN_POINT ( 'NONE',  ( 0.000000000000000000, 0.000000000000000000, -11.12471428571428689 ) ) ;
#43015=EDGE_LOOP ( 'NONE', ( #78706, #44162, #1116 ) ) ;
#43037=DIRECTION ( 'NONE',  ( -1.000000000000000000, 0.000000000000000000, 0.000000000000000000 ) ) ;
#43068=CARTESIAN_POINT ( 'NONE',  ( 0.000000000000000000, 0.000000000000000000, -11.12471428571428689 ) ) ;
#43077=EDGE_CURVE ( 'NONE', #34348, #56853, #76304, .T. ) ;
#43094=ADVANCED_FACE ( 'NONE', ( #93574 ), #15325, .F. ) ;
#43318=ORIENTED_EDGE ( 'NONE', *, *, #4531, .F. ) ;
#43374=EDGE_LOOP ( 'NONE', ( #80450, #11968, #70529, #80420 ) ) ;
#43491=LINE ( 'NONE', #2480, #45668 ) ;
#43522=DIRECTION ( 'NONE',  ( -0.000000000000000000, -0.000000000000000000, 1.000000000000000000 ) ) ;
#43562=CARTESIAN_POINT ( 'NONE',  ( 6.750000000000016875, -11.69134295108991495, 0.000000000000000000 ) ) ;
#43613=CARTESIAN_POINT ( 'NONE',  ( 13.50000000000000355, 7.794228634059934713, -13.00000000000000000 ) ) ;
#43679=ORIENTED_EDGE ( 'NONE', *, *, #3372, .F. ) ;
#43772=( GEOMETRIC_REPRESENTATION_CONTEXT ( 3 ) GLOBAL_UNCERTAINTY_ASSIGNED_CONTEXT ( ( #58605 ) ) GLOBAL_UNIT_ASSIGNED_CONTEXT ( ( #86808, #18905, #85748 ) ) REPRESENTATION_CONTEXT ( 'NONE', 'WORKASPACE' ) );
#43792=DIRECTION ( 'NONE',  ( 1.000000000000000000, 0.000000000000000000, 0.000000000000000000 ) ) ;
#43829=EDGE_CURVE ( 'NONE', #38464, #92662, #3088, .T. ) ;
#43997=EDGE_CURVE ( 'NONE', #92662, #38464, #40966, .T. ) ;
#44045=EDGE_CURVE ( 'NONE', #60134, #1766, #54729, .T. ) ;
#44133=ORIENTED_EDGE ( 'NONE', *, *, #29269, .T. ) ;
#44162=ORIENTED_EDGE ( 'NONE', *, *, #22955, .T. ) ;
#44179=DIRECTION ( 'NONE',  ( 1.000000000000000000, 0.000000000000000000, 0.000000000000000000 ) ) ;
#44183=VERTEX_POINT ( 'NONE', #51768 ) ;
#44265=VECTOR ( 'NONE', #99540, 1000.000000000000000 ) ;
#44273=VERTEX_POINT ( 'NONE', #43562 ) ;
#44365=AXIS2_PLACEMENT_3D ( 'NONE', #100802, #26961, #44179 ) ;
#44380=EDGE_CURVE ( 'NONE', #71627, #56853, #39294, .T. ) ;
#44401=ORIENTED_EDGE ( 'NONE', *, *, #71600, .T. ) ;
#44515=ADVANCED_FACE ( 'NONE', ( #82289 ), #73753, .F. ) ;
#44579=ORIENTED_EDGE ( 'NONE', *, *, #32107, .T. ) ;
#44608=FACE_OUTER_BOUND ( 'NONE', #79580, .T. ) ;
#44729=ADVANCED_FACE ( 'NONE', ( #89072 ), #538, .F. ) ;
#44750=EDGE_CURVE ( 'NONE', #3475, #60873, #91099, .T. ) ;
#44840=CARTESIAN_POINT ( 'NONE',  ( 9.601913782316094270, 10.04478976116411459, -0.2204769333330966474 ) ) ;
#44879=DIRECTION ( 'NONE',  ( 0.000000000000000000, 0.000000000000000000, 1.000000000000000000 ) ) ;
#44907=VERTEX_POINT ( 'NONE', #38296 ) ;
#44908=EDGE_CURVE ( 'NONE', #16577, #95900, #29681, .T. ) ;
#45031=DIRECTION ( 'NONE',  ( -0.000000000000000000, -0.000000000000000000, -1.000000000000000000 ) ) ;
#45045=FACE_OUTER_BOUND ( 'NONE', #21827, .T. ) ;
#45198=CARTESIAN_POINT ( 'NONE',  ( 0.000000000000000000, 0.000000000000000000, -5.575057142857143155 ) ) ;
#45233=CARTESIAN_POINT ( 'NONE',  ( -7.000000000000000000, 8.572527594031471218E-16, -4.874849604647447876 ) ) ;
#45243=DIRECTION ( 'NONE',  ( -0.8660254037844379305, -0.5000000000000014433, 0.000000000000000000 ) ) ;
#45393=EDGE_CURVE ( 'NONE', #21224, #30181, #58439, .T. ) ;
#45413=AXIS2_PLACEMENT_3D ( 'NONE', #30253, #55016, #28681 ) ;
#45424=DIRECTION ( 'NONE',  ( -1.000000000000000000, 0.000000000000000000, 0.000000000000000000 ) ) ;
#45435=CARTESIAN_POINT ( 'NONE',  ( 7.000000000000000000, 0.000000000000000000, -13.00000000000000000 ) ) ;
#45461=ADVANCED_FACE ( 'NONE', ( #14909 ), #101552, .F. ) ;
#45564=EDGE_LOOP ( 'NONE', ( #27785, #73910, #12256, #100774 ) ) ;
#45596=EDGE_LOOP ( 'NONE', ( #77039, #11297, #91784, #86115 ) ) ;
#45639=CARTESIAN_POINT ( 'NONE',  ( -12.39578842395470915, 8.431745484731985485, -0.8377008405913517475 ) ) ;
#45668=VECTOR ( 'NONE', #92030, 1000.000000000000000 ) ;
#45906=ADVANCED_FACE ( 'NONE', ( #16666 ), #86114, .T. ) ;
#45916=PRODUCT_DEFINITION_SHAPE ( 'NONE', 'NONE',  #103634 ) ;
#45983=EDGE_CURVE ( 'NONE', #32846, #3555, #18988, .T. ) ;
#46002=CARTESIAN_POINT ( 'NONE',  ( 5.601730134768061475, -12.35429686688396522, -0.02849990174191881914 ) ) ;
#46004=DIRECTION ( 'NONE',  ( -1.000000000000000000, 0.000000000000000000, 0.000000000000000000 ) ) ;
#46013=EDGE_LOOP ( 'NONE', ( #102454, #97610, #90971, #24102 ) ) ;
#46018=ORIENTED_EDGE ( 'NONE', *, *, #19938, .T. ) ;
#46196=EDGE_CURVE ( 'NONE', #79592, #18742, #67228, .T. ) ;
#46220=CARTESIAN_POINT ( 'NONE',  ( -6.750000000000018652, 11.69134295108991317, 0.000000000000000000 ) ) ;
#46242=CARTESIAN_POINT ( 'NONE',  ( -13.50000000000000178, 1.319989657865592303, -0.02800283339254916112 ) ) ;
#46285=ORIENTED_EDGE ( 'NONE', *, *, #44380, .F. ) ;
#46365=DIRECTION ( 'NONE',  ( 0.8191520442889974607, 1.003171929053531649E-16, -0.5735764363510380548 ) ) ;
#46405=UNCERTAINTY_MEASURE_WITH_UNIT (LENGTH_MEASURE( 1.000000000000000082E-05 ), #3078, 'distance_accuracy_value', 'NONE');
#46488=DIRECTION ( 'NONE',  ( 1.000000000000000000, 0.000000000000000000, 0.000000000000000000 ) ) ;
#46662=EDGE_LOOP ( 'NONE', ( #52027, #56273, #21104 ) ) ;
#46685=DIRECTION ( 'NONE',  ( -1.000000000000000000, 0.000000000000000000, 0.000000000000000000 ) ) ;
#46695=ORIENTED_EDGE ( 'NONE', *, *, #66782, .F. ) ;
#46745=EDGE_LOOP ( 'NONE', ( #25203, #86096, #30938, #9061 ) ) ;
#46789=CARTESIAN_POINT ( 'NONE',  ( 0.000000000000000000, 0.000000000000000000, -6.275264681066861527 ) ) ;
#46883=DIRECTION ( 'NONE',  ( -0.000000000000000000, -0.000000000000000000, -1.000000000000000000 ) ) ;
#46897=CARTESIAN_POINT ( 'NONE',  ( 0.000000000000000000, 0.000000000000000000, 0.000000000000000000 ) ) ;
#46934=CARTESIAN_POINT ( 'NONE',  ( 0.000000000000000000, 0.000000000000000000, -13.00000000000000000 ) ) ;
#47015=CARTESIAN_POINT ( 'NONE',  ( -13.49999999999999645, 0.000000000000000000, -13.00000000000000000 ) ) ;
#47070=EDGE_LOOP ( 'NONE', ( #40520, #19168, #80457, #73464 ) ) ;
#47079=AXIS2_PLACEMENT_3D ( 'NONE', #76533, #60389, #77616 ) ;
#47213=ORIENTED_EDGE ( 'NONE', *, *, #80554, .T. ) ;
#47310=PLANE ( 'NONE',  #78070 ) ;
#47327=ORIENTED_EDGE ( 'NONE', *, *, #87673, .T. ) ;
#47352=CARTESIAN_POINT ( 'NONE',  ( 0.000000000000000000, 0.000000000000000000, -13.00000000000000000 ) ) ;
#47413=VERTEX_POINT ( 'NONE', #70023 ) ;
#47418=VERTEX_POINT ( 'NONE', #45233 ) ;
#47428=EDGE_CURVE ( 'NONE', #91520, #3430, #20993, .T. ) ;
#47519=DIRECTION ( 'NONE',  ( -1.000000000000000000, 0.000000000000000000, 0.000000000000000000 ) ) ;
#47653=CARTESIAN_POINT ( 'NONE',  ( 0.000000000000000000, 0.000000000000000000, -5.575057142857143155 ) ) ;
#47654=ORIENTED_EDGE ( 'NONE', *, *, #87921, .F. ) ;
#47666=AXIS2_PLACEMENT_3D ( 'NONE', #38966, #22269, #13599 ) ;
#47766=CARTESIAN_POINT ( 'NONE',  ( 7.000000000000000000, 0.000000000000000000, -8.125150395352576993 ) ) ;
#47878=DIRECTION ( 'NONE',  ( 1.000000000000000000, 0.000000000000000000, 0.000000000000000000 ) ) ;
#47915=CARTESIAN_POINT ( 'NONE',  ( -13.50000000000000000, -7.794228634059985339, -11.79422863405993382 ) ) ;
#47952=B_SPLINE_CURVE_WITH_KNOTS ( 'NONE', 3,
 ( #90701, #42672, #1666, #75571, #24403, #83132 ),
 .UNSPECIFIED., .F., .F.,
 ( 4, 2, 4 ),
 ( 2.380729205304141141E-07, 0.003943479449179690573, 0.007886720825438852528 ),
 .UNSPECIFIED. ) ;
#47986=CARTESIAN_POINT ( 'NONE',  ( 13.50000000000000355, -1.317096457811609111, -1.029992063861229212E-15 ) ) ;
#47994=CIRCLE ( 'NONE', #42858, 8.000000000000000000 ) ;
#48028=ADVANCED_FACE ( 'NONE', ( #73590 ), #37479, .F. ) ;
#48033=VECTOR ( 'NONE', #53106, 999.9999999999998863 ) ;
#48056=CARTESIAN_POINT ( 'NONE',  ( 0.000000000000000000, 0.000000000000000000, -13.00000000000000000 ) ) ;
#48075=VECTOR ( 'NONE', #73222, 1000.000000000000000 ) ;
#48098=DIRECTION ( 'NONE',  ( 0.8191520442889884679, 0.000000000000000000, 0.5735764363510509334 ) ) ;
#48163=CARTESIAN_POINT ( 'NONE',  ( -8.000000000000000000, 0.000000000000000000, -1.875285714285714445 ) ) ;
#48296=CARTESIAN_POINT ( 'NONE',  ( 13.50000000000000355, 6.533945317241105499, -0.8419589098297789453 ) ) ;
#48433=VECTOR ( 'NONE', #50567, 1000.000000000000000 ) ;
#48442=CARTESIAN_POINT ( 'NONE',  ( -6.750000000000015099, -11.69134295108991495, 0.000000000000000000 ) ) ;
#48492=LINE ( 'NONE', #56040, #92566 ) ;
#48571=DIRECTION ( 'NONE',  ( 0.000000000000000000, -0.000000000000000000, 1.000000000000000000 ) ) ;
#48579=FACE_BOUND ( 'NONE', #106499, .T. ) ;
#48582=ADVANCED_FACE ( 'NONE', ( #19949 ), #10200, .F. ) ;
#48596=ORIENTED_EDGE ( 'NONE', *, *, #10204, .F. ) ;
#48779=CYLINDRICAL_SURFACE ( 'NONE', #63384, 7.000000000000000000 ) ;
#48905=CARTESIAN_POINT ( 'NONE',  ( 12.39578842395471803, -8.431745484732024565, -0.8377008405913674016 ) ) ;
#48967=B_SPLINE_CURVE_WITH_KNOTS ( 'NONE', 3,
 ( #5048, #37981, #27774, #20215, #85435, #61716, #11517, #12060 ),
 .UNSPECIFIED., .F., .F.,
 ( 4, 2, 2, 4 ),
 ( 0.007886720825438776200, 0.009850969036564001177, 0.01181521724768922615, 0.01574371366993967264 ),
 .UNSPECIFIED. ) ;
#49012=CARTESIAN_POINT ( 'NONE',  ( 0.000000000000000000, 0.000000000000000000, -13.00000000000000000 ) ) ;
#49038=ORIENTED_EDGE ( 'NONE', *, *, #35850, .T. ) ;
#49074=EDGE_LOOP ( 'NONE', ( #51413, #38724, #34385, #75733 ) ) ;
#49123=AXIS2_PLACEMENT_3D ( 'NONE', #17955, #92886, #68642 ) ;
#49146=CARTESIAN_POINT ( 'NONE',  ( -13.49999999999999822, -6.526560492696116711, -0.8398270946102923684 ) ) ;
#49158=LINE ( 'NONE', #8184, #63302 ) ;
#49168=DIRECTION ( 'NONE',  ( -1.000000000000000000, 0.000000000000000000, 0.000000000000000000 ) ) ;
#49194=ORIENTED_EDGE ( 'NONE', *, *, #62511, .T. ) ;
#49334=AXIS2_PLACEMENT_3D ( 'NONE', #42980, #85578, #76388 ) ;
#49411=ORIENTED_EDGE ( 'NONE', *, *, #45393, .F. ) ;
#49447=CARTESIAN_POINT ( 'NONE',  ( 8.000000000000000000, 9.797174393178825657E-16, -1.875285714285714445 ) ) ;
#49473=ADVANCED_FACE ( 'NONE', ( #10973 ), #13796, .F. ) ;
#49477=ORIENTED_EDGE ( 'NONE', *, *, #69142, .F. ) ;
#49540=ORIENTED_EDGE ( 'NONE', *, *, #46196, .T. ) ;
#49631=CARTESIAN_POINT ( 'NONE',  ( -6.750000000000015099, -11.69134295108991495, 0.000000000000000000 ) ) ;
#49705=DIRECTION ( 'NONE',  ( 0.000000000000000000, 0.000000000000000000, 1.000000000000000000 ) ) ;
#49713=CIRCLE ( 'NONE', #39425, 8.000000000000000000 ) ;
#49772=LINE ( 'NONE', #9299, #74036 ) ;
#49830=CARTESIAN_POINT ( 'NONE',  ( 7.898269865231975828, 11.02838903529590908, -12.97150009825809924 ) ) ;
#49876=AXIS2_PLACEMENT_3D ( 'NONE', #18331, #68464, #9662 ) ;
#49905=AXIS2_PLACEMENT_3D ( 'NONE', #94635, #68766, #93561 ) ;
#49999=ORIENTED_EDGE ( 'NONE', *, *, #31655, .F. ) ;
#50065=VERTEX_POINT ( 'NONE', #84508 ) ;
#50071=AXIS2_PLACEMENT_3D ( 'NONE', #70803, #96146, #13075 ) ;
#50132=ORIENTED_EDGE ( 'NONE', *, *, #60282, .T. ) ;
#50170=CONICAL_SURFACE ( 'NONE', #20979, 7.000000000000000000, 0.9599310885968753704 ) ;
#50190=DIRECTION ( 'NONE',  ( -0.000000000000000000, -0.000000000000000000, -1.000000000000000000 ) ) ;
#50193=DIRECTION ( 'NONE',  ( -0.000000000000000000, -0.000000000000000000, -1.000000000000000000 ) ) ;
#50283=DIRECTION ( 'NONE',  ( -1.000000000000000000, 0.000000000000000000, 0.000000000000000000 ) ) ;
#50408=EDGE_CURVE ( 'NONE', #21504, #3430, #31238, .T. ) ;
#50431=DIRECTION ( 'NONE',  ( -1.000000000000000000, 0.000000000000000000, 0.000000000000000000 ) ) ;
#50432=CARTESIAN_POINT ( 'NONE',  ( 7.000000000000000000, 0.000000000000000000, -13.00000000000000000 ) ) ;
#50474=CARTESIAN_POINT ( 'NONE',  ( -13.50000000000000000, 7.794228634059985339, -11.79422863405993382 ) ) ;
#50532=EDGE_LOOP ( 'NONE', ( #14670, #17349, #36936, #14727 ) ) ;
#50567=DIRECTION ( 'NONE',  ( 0.8191520442889974607, 1.003171929053531649E-16, -0.5735764363510380548 ) ) ;
#50687=EDGE_CURVE ( 'NONE', #17308, #21504, #5052, .T. ) ;
#50795=CARTESIAN_POINT ( 'NONE',  ( 0.000000000000000000, 0.000000000000000000, 0.000000000000000000 ) ) ;
#50869=VERTEX_POINT ( 'NONE', #34135 ) ;
#50927=EDGE_LOOP ( 'NONE', ( #19366, #72168, #46285, #78199 ) ) ;
#50962=CARTESIAN_POINT ( 'NONE',  ( 0.000000000000000000, 0.000000000000000000, -3.725171428571429022 ) ) ;
#51143=EDGE_CURVE ( 'NONE', #47418, #9380, #81434, .T. ) ;
#51155=DIRECTION ( 'NONE',  ( 1.000000000000000000, 0.000000000000000000, 0.000000000000000000 ) ) ;
#51172=AXIS2_PLACEMENT_3D ( 'NONE', #91823, #2796, #50283 ) ;
#51313=CARTESIAN_POINT ( 'NONE',  ( 0.000000000000000000, 0.000000000000000000, 0.000000000000000000 ) ) ;
#51413=ORIENTED_EDGE ( 'NONE', *, *, #100169, .F. ) ;
#51464=CLOSED_SHELL ( 'NONE', ( #55595, #45461, #13524, #25018, #6905, #83790, #24559, #32816, #7930, #79129, #93682, #58735, #92572, #96621, #26855, #30588, #13791, #48582, #38349, #82652, #26313, #105614, #91090, #89320, #95172, #20570, #44729, #95319, #23393, #30919, #94217, #102983, #54128, #58959, #69939, #99356, #9762, #75951, #53879, #534, #91150, #86386, #97535, #45906, #8176, #37275, #65038, #5893, #39780, #8012, #1439, #53683, #66635, #40611, #101124, #48028, #43094, #59092, #52690, #11451, #68486, #49473, #10396, #44515, #18065, #104144, #12053, #77489 ) ) ;
#51490=B_SPLINE_CURVE_WITH_KNOTS ( 'NONE', 3,
 ( #103855, #45639, #14299, #38107, #21386, #12717 ),
 .UNSPECIFIED., .F., .F.,
 ( 4, 2, 4 ),
 ( 2.380729204614878139E-07, 0.003943479449179625521, 0.007886720825438788343 ),
 .UNSPECIFIED. ) ;
#51516=ORIENTED_EDGE ( 'NONE', *, *, #2080, .T. ) ;
#51583=ORIENTED_EDGE ( 'NONE', *, *, #101021, .F. ) ;
#51716=CARTESIAN_POINT ( 'NONE',  ( -13.50000000000000000, -7.794228634059985339, -1.205771365940065953 ) ) ;
#51765=DIRECTION ( 'NONE',  ( 1.000000000000000000, 0.000000000000000000, 0.000000000000000000 ) ) ;
#51768=CARTESIAN_POINT ( 'NONE',  ( -13.50000000000000000, 7.794228634059985339, -11.79422863405993382 ) ) ;
#51769=CARTESIAN_POINT ( 'NONE',  ( 0.000000000000000000, 0.000000000000000000, -6.724735318933162453 ) ) ;
#51860=CARTESIAN_POINT ( 'NONE',  ( 7.000000000000000000, 0.000000000000000000, -6.275264681066861527 ) ) ;
#51890=B_SPLINE_CURVE_WITH_KNOTS ( 'NONE', 3,
 ( #100045, #73088, #56379, #89313, #7838, #15408, #48296, #81194 ),
 .UNSPECIFIED., .F., .F.,
 ( 4, 2, 2, 4 ),
 ( 0.02179091314793462145, 0.02376333058066962267, 0.02573574801340462737, 0.02968058287887462982 ),
 .UNSPECIFIED. ) ;
#51918=EDGE_CURVE ( 'NONE', #34061, #92662, #34451, .T. ) ;
#51953=DIRECTION ( 'NONE',  ( -0.8191520442889974607, 0.000000000000000000, -0.5735764363510380548 ) ) ;
#52005=DIRECTION ( 'NONE',  ( 1.000000000000000000, 0.000000000000000000, 0.000000000000000000 ) ) ;
#52027=ORIENTED_EDGE ( 'NONE', *, *, #23962, .T. ) ;
#52081=CARTESIAN_POINT ( 'NONE',  ( -12.39578842395469138, 8.431745484731994367, -12.16229915940865070 ) ) ;
#52086=DIRECTION ( 'NONE',  ( 0.000000000000000000, 0.000000000000000000, -1.000000000000000000 ) ) ;
#52133=CARTESIAN_POINT ( 'NONE',  ( 13.50000000000000533, -7.794228634059982674, -11.79422863405993382 ) ) ;
#52201=CARTESIAN_POINT ( 'NONE',  ( -13.50000000000000178, 0.6589394956329809316, -13.00000000000000178 ) ) ;
#52296=DIRECTION ( 'NONE',  ( 0.8191520442889884679, 0.000000000000000000, 0.5735764363510509334 ) ) ;
#52306=ORIENTED_EDGE ( 'NONE', *, *, #52882, .F. ) ;
#52630=CARTESIAN_POINT ( 'NONE',  ( 0.000000000000000000, 0.000000000000000000, -0.02540000000000007530 ) ) ;
#52643=VERTEX_POINT ( 'NONE', #42108 ) ;
#52690=ADVANCED_FACE ( 'NONE', ( #94405 ), #59162, .F. ) ;
#52847=DIRECTION ( 'NONE',  ( 1.000000000000000000, 0.000000000000000000, 0.000000000000000000 ) ) ;
#52882=EDGE_CURVE ( 'NONE', #32906, #70854, #580, .T. ) ;
#52940=AXIS2_PLACEMENT_3D ( 'NONE', #53502, #12490, #45424 ) ;
#53074=ORIENTED_EDGE ( 'NONE', *, *, #98376, .F. ) ;
#53106=DIRECTION ( 'NONE',  ( -0.8191520442889884679, 1.003171929053520679E-16, 0.5735764363510509334 ) ) ;
#53118=EDGE_CURVE ( 'NONE', #23867, #1766, #15370, .T. ) ;
#53139=PLANE ( 'NONE',  #84360 ) ;
#53156=CIRCLE ( 'NONE', #3183, 13.50000000000000000 ) ;
#53275=DIRECTION ( 'NONE',  ( -1.000000000000000000, 0.000000000000000000, 0.000000000000000000 ) ) ;
#53277=ORIENTED_EDGE ( 'NONE', *, *, #51918, .F. ) ;
#53376=CONICAL_SURFACE ( 'NONE', #70390, 8.000000000000000000, 0.9599310885968911355 ) ;
#53397=DIRECTION ( 'NONE',  ( 0.8191520442889974607, 1.003171929053531649E-16, -0.5735764363510380548 ) ) ;
#53406=DIRECTION ( 'NONE',  ( -1.000000000000000000, 0.000000000000000000, 0.000000000000000000 ) ) ;
#53502=CARTESIAN_POINT ( 'NONE',  ( 0.000000000000000000, 0.000000000000000000, -8.125150395352576993 ) ) ;
#53520=DIRECTION ( 'NONE',  ( 0.000000000000000000, 0.000000000000000000, 1.000000000000000000 ) ) ;
#53646=B_SPLINE_CURVE_WITH_KNOTS ( 'NONE', 3,
 ( #35175, #59441, #4776, #21007, #5313, #70037 ),
 .UNSPECIFIED., .F., .F.,
 ( 4, 2, 4 ),
 ( 2.380729204593255505E-07, 0.003943479449179646337, 0.007886720825438833446 ),
 .UNSPECIFIED. ) ;
#53668=DIRECTION ( 'NONE',  ( -0.000000000000000000, -0.000000000000000000, -1.000000000000000000 ) ) ;
#53683=ADVANCED_FACE ( 'NONE', ( #90560 ), #53887, .F. ) ;
#53689=CARTESIAN_POINT ( 'NONE',  ( 1.104211576045296406, 14.95094041744785329, -12.16229915940863293 ) ) ;
#53818=ORIENTED_EDGE ( 'NONE', *, *, #56578, .T. ) ;
#53828=EDGE_CURVE ( 'NONE', #52643, #32906, #85128, .T. ) ;
#53879=ADVANCED_FACE ( 'NONE', ( #75967, #11213 ), #2064, .T. ) ;
#53886=CARTESIAN_POINT ( 'NONE',  ( -2.212097561415797387, 14.31130214556278268, -12.46447053051441678 ) ) ;
#53887=CONICAL_SURFACE ( 'NONE', #14229, 6.900000000000000355, 0.9599310885968801443 ) ;
#53971=CARTESIAN_POINT ( 'NONE',  ( -13.50000000000000178, -1.317096457811610888, -13.00000000000000178 ) ) ;
#54010=DIRECTION ( 'NONE',  ( -1.000000000000000000, 0.000000000000000000, 0.000000000000000000 ) ) ;
#54012=DIRECTION ( 'NONE',  ( 0.000000000000000000, 0.000000000000000000, 1.000000000000000000 ) ) ;
#54058=CARTESIAN_POINT ( 'NONE',  ( 6.177150199754223969, -12.02207793746708830, -1.226588410918951848E-14 ) ) ;
#54105=CARTESIAN_POINT ( 'NONE',  ( -7.000000000000000000, 8.572527594031471218E-16, -13.00000000000000000 ) ) ;
#54128=ADVANCED_FACE ( 'NONE', ( #96933 ), #47310, .T. ) ;
#54162=VECTOR ( 'NONE', #2391, 1000.000000000000000 ) ;
#54199=ORIENTED_EDGE ( 'NONE', *, *, #86921, .F. ) ;
#54224=ORIENTED_EDGE ( 'NONE', *, *, #17507, .T. ) ;
#54466=AXIS2_PLACEMENT_3D ( 'NONE', #75492, #34548, #65814 ) ;
#54661=B_SPLINE_CURVE_WITH_KNOTS ( 'NONE', 3,
 ( #16805, #49146, #41610, #33015, #1114, #17883 ),
 .UNSPECIFIED., .F., .F.,
 ( 4, 2, 4 ),
 ( 0.01390592816464531790, 0.01784842065628996707, 0.02179091314793461798 ),
 .UNSPECIFIED. ) ;
#54729=CIRCLE ( 'NONE', #68543, 13.50000000000000000 ) ;
#54760=CARTESIAN_POINT ( 'NONE',  ( 0.000000000000000000, 0.000000000000000000, -10.42450674750459072 ) ) ;
#54789=AXIS2_PLACEMENT_3D ( 'NONE', #67868, #84051, #3675 ) ;
#54940=CARTESIAN_POINT ( 'NONE',  ( -3.898086217683917276, 13.33789614101572418, -12.77952306666689886 ) ) ;
#54941=AXIS2_PLACEMENT_3D ( 'NONE', #77666, #69050, #52847 ) ;
#54966=ORIENTED_EDGE ( 'NONE', *, *, #71544, .F. ) ;
#55015=CARTESIAN_POINT ( 'NONE',  ( 13.50000000000000533, -7.794228634059977345, -1.205771365940065953 ) ) ;
#55016=DIRECTION ( 'NONE',  ( 0.000000000000000000, -0.000000000000000000, 1.000000000000000000 ) ) ;
#55032=CARTESIAN_POINT ( 'NONE',  ( -13.50000000000000000, -7.794228634059985339, -11.79422863405993382 ) ) ;
#55057=ORIENTED_EDGE ( 'NONE', *, *, #24679, .T. ) ;
#55082=EDGE_CURVE ( 'NONE', #42431, #64475, #77795, .T. ) ;
#55120=ORIENTED_EDGE ( 'NONE', *, *, #2297, .T. ) ;
#55127=CARTESIAN_POINT ( 'NONE',  ( 0.000000000000000000, 0.000000000000000000, -12.27439246179028309 ) ) ;
#55318=CARTESIAN_POINT ( 'NONE',  ( 0.000000000000000000, 0.000000000000000000, -3.024963890361733743 ) ) ;
#55408=DIRECTION ( 'NONE',  ( 0.000000000000000000, 0.000000000000000000, 1.000000000000000000 ) ) ;
#55595=ADVANCED_FACE ( 'NONE', ( #28087 ), #21435, .F. ) ;
#55598=ORIENTED_EDGE ( 'NONE', *, *, #36833, .T. ) ;
#55637=ORIENTED_EDGE ( 'NONE', *, *, #104139, .F. ) ;
#55687=DIRECTION ( 'NONE',  ( 0.000000000000000000, 0.000000000000000000, 1.000000000000000000 ) ) ;
#55780=ORIENTED_EDGE ( 'NONE', *, *, #79789, .F. ) ;
#55839=DIRECTION ( 'NONE',  ( -0.000000000000000000, -0.000000000000000000, -1.000000000000000000 ) ) ;
#56040=CARTESIAN_POINT ( 'NONE',  ( -13.50000000000000000, 7.794228634059933825, -13.00000000000000000 ) ) ;
#56063=CARTESIAN_POINT ( 'NONE',  ( -8.000000000000000000, 0.000000000000000000, -11.12471428571428689 ) ) ;
#56165=CARTESIAN_POINT ( 'NONE',  ( 13.50000000000000533, -7.794228634059977345, -1.205771365940065953 ) ) ;
#56174=CARTESIAN_POINT ( 'NONE',  ( 7.000000000000000000, 0.000000000000000000, -4.425378966781146950 ) ) ;
#56251=EDGE_CURVE ( 'NONE', #2886, #38464, #41586, .T. ) ;
#56273=ORIENTED_EDGE ( 'NONE', *, *, #53118, .T. ) ;
#56379=CARTESIAN_POINT ( 'NONE',  ( 13.50000000000000355, 1.319989657865598298, -0.02800283339255059054 ) ) ;
#56403=VERTEX_POINT ( 'NONE', #10794 ) ;
#56537=CARTESIAN_POINT ( 'NONE',  ( -2.212097561415799163, 14.31130214556278268, -0.5355294694855831095 ) ) ;
#56551=EDGE_LOOP ( 'NONE', ( #84177, #55120, #37269, #82245, #88918, #24230 ) ) ;
#56559=ORIENTED_EDGE ( 'NONE', *, *, #82149, .F. ) ;
#56578=EDGE_CURVE ( 'NONE', #60134, #44183, #74199, .T. ) ;
#56582=DIRECTION ( 'NONE',  ( -0.000000000000000000, -0.000000000000000000, 1.000000000000000000 ) ) ;
#56587=ORIENTED_EDGE ( 'NONE', *, *, #31341, .F. ) ;
#56853=VERTEX_POINT ( 'NONE', #5779 ) ;
#56869=CYLINDRICAL_SURFACE ( 'NONE', #12479, 7.000000000000000000 ) ;
#57027=EDGE_CURVE ( 'NONE', #96238, #30181, #105536, .T. ) ;
#57033=DIRECTION ( 'NONE',  ( 0.000000000000000000, 0.000000000000000000, 1.000000000000000000 ) ) ;
#57298=ORIENTED_EDGE ( 'NONE', *, *, #22285, .T. ) ;
#57369=EDGE_CURVE ( 'NONE', #20513, #102378, #42413, .T. ) ;
#57382=CARTESIAN_POINT ( 'NONE',  ( 7.322849800245819551, 11.36060796471277712, -13.00000000000000711 ) ) ;
#57436=DIRECTION ( 'NONE',  ( 1.000000000000000000, 0.000000000000000000, 0.000000000000000000 ) ) ;
#57565=AXIS2_PLACEMENT_3D ( 'NONE', #88808, #64540, #63488 ) ;
#57587=CARTESIAN_POINT ( 'NONE',  ( -7.000000000000000000, 8.572527594031471218E-16, -10.42450674750459072 ) ) ;
#57722=AXIS2_PLACEMENT_3D ( 'NONE', #26597, #93423, #76154 ) ;
#57813=EDGE_CURVE ( 'NONE', #88199, #24805, #17494, .T. ) ;
#57827=DIRECTION ( 'NONE',  ( -1.000000000000000000, 0.000000000000000000, 0.000000000000000000 ) ) ;
#58037=CIRCLE ( 'NONE', #71741, 8.000000000000000000 ) ;
#58171=CARTESIAN_POINT ( 'NONE',  ( 0.000000000000000000, 0.000000000000000000, -25.03750572909317285 ) ) ;
#58198=CARTESIAN_POINT ( 'NONE',  ( -6.750000000000015099, -11.69134295108991495, -13.00000000000000000 ) ) ;
#58210=FACE_OUTER_BOUND ( 'NONE', #45596, .T. ) ;
#58232=VECTOR ( 'NONE', #40630, 999.9999999999998863 ) ;
#58271=DIRECTION ( 'NONE',  ( -1.000000000000000000, 0.000000000000000000, 0.000000000000000000 ) ) ;
#58297=DIRECTION ( 'NONE',  ( 0.8191520442889974607, 1.003171929053531649E-16, -0.5735764363510380548 ) ) ;
#58320=CIRCLE ( 'NONE', #60050, 13.50000000000000000 ) ;
#58364=VERTEX_POINT ( 'NONE', #46220 ) ;
#58368=CONICAL_SURFACE ( 'NONE', #60094, 13.50000000000000178, 1.047197551196596077 ) ;
#58439=CIRCLE ( 'NONE', #84304, 8.000000000000000000 ) ;
#58536=DIRECTION ( 'NONE',  ( 0.000000000000000000, 0.000000000000000000, 1.000000000000000000 ) ) ;
#58588=LINE ( 'NONE', #10022, #9759 ) ;
#58605=UNCERTAINTY_MEASURE_WITH_UNIT (LENGTH_MEASURE( 1.000000000000000082E-05 ), #86808, 'distance_accuracy_value', 'NONE');
#58699=CARTESIAN_POINT ( 'NONE',  ( -6.177150199754213311, 12.02207793746705278, 8.529057090219303651E-15 ) ) ;
#58717=ORIENTED_EDGE ( 'NONE', *, *, #24728, .T. ) ;
#58724=FACE_OUTER_BOUND ( 'NONE', #92125, .T. ) ;
#58735=ADVANCED_FACE ( 'NONE', ( #45045 ), #8135, .F. ) ;
#58846=AXIS2_PLACEMENT_3D ( 'NONE', #24877, #90656, #7069 ) ;
#58959=ADVANCED_FACE ( 'NONE', ( #25016 ), #41178, .F. ) ;
#58964=DIRECTION ( 'NONE',  ( -1.000000000000000000, 0.000000000000000000, 0.000000000000000000 ) ) ;
#58968=DIRECTION ( 'NONE',  ( -1.000000000000000000, 0.000000000000000000, 0.000000000000000000 ) ) ;
#58987=VERTEX_POINT ( 'NONE', #8799 ) ;
#59034=ORIENTED_EDGE ( 'NONE', *, *, #53828, .F. ) ;
#59046=CARTESIAN_POINT ( 'NONE',  ( -7.000000000000000000, 8.572527594031471218E-16, -13.00000000000000000 ) ) ;
#59075=EDGE_LOOP ( 'NONE', ( #13657, #70243 ) ) ;
#59092=ADVANCED_FACE ( 'NONE', ( #20679 ), #103008, .F. ) ;
#59162=CONICAL_SURFACE ( 'NONE', #12622, 8.000000000000000000, 0.9599310885968911355 ) ;
#59291=DIRECTION ( 'NONE',  ( -1.000000000000000000, 0.000000000000000000, 0.000000000000000000 ) ) ;
#59312=ORIENTED_EDGE ( 'NONE', *, *, #77865, .F. ) ;
#59427=EDGE_CURVE ( 'NONE', #99841, #23394, #59642, .T. ) ;
#59433=CARTESIAN_POINT ( 'NONE',  ( 0.000000000000000000, 0.000000000000000000, -6.275264681066861527 ) ) ;
#59441=CARTESIAN_POINT ( 'NONE',  ( 1.104211576045294407, 14.95094041744785862, -0.8377008405913628497 ) ) ;
#59481=PLANE ( 'NONE',  #49123 ) ;
#59482=DIRECTION ( 'NONE',  ( -0.000000000000000000, -0.000000000000000000, 1.000000000000000000 ) ) ;
#59642=LINE ( 'NONE', #92516, #44265 ) ;
#59701=VECTOR ( 'NONE', #67003, 999.9999999999998863 ) ;
#59736=AXIS2_PLACEMENT_3D ( 'NONE', #21798, #22328, #14183 ) ;
#59787=AXIS2_PLACEMENT_3D ( 'NONE', #52630, #27358, #83409 ) ;
#59969=CARTESIAN_POINT ( 'NONE',  ( 13.50000000000000355, 7.794228634059978233, -1.205771365940065953 ) ) ;
#60026=FACE_OUTER_BOUND ( 'NONE', #31388, .T. ) ;
#60050=AXIS2_PLACEMENT_3D ( 'NONE', #8438, #74231, #33275 ) ;
#60077=EDGE_LOOP ( 'NONE', ( #75456, #16157, #78668, #71156 ) ) ;
#60094=AXIS2_PLACEMENT_3D ( 'NONE', #24731, #5858, #7438 ) ;
#60103=AXIS2_PLACEMENT_3D ( 'NONE', #77916, #45031, #18639 ) ;
#60134=VERTEX_POINT ( 'NONE', #47015 ) ;
#60221=CARTESIAN_POINT ( 'NONE',  ( 4.464296094009049476, 13.01099471650158002, -12.88508357975252139 ) ) ;
#60282=EDGE_CURVE ( 'NONE', #31665, #25443, #13283, .T. ) ;
#60300=CARTESIAN_POINT ( 'NONE',  ( -12.39854599882998976, -8.430153398135471932, -0.8386200322165905385 ) ) ;
#60389=DIRECTION ( 'NONE',  ( 0.000000000000000000, -0.000000000000000000, 1.000000000000000000 ) ) ;
#60433=DIRECTION ( 'NONE',  ( -0.000000000000000000, -0.000000000000000000, -1.000000000000000000 ) ) ;
#60494=CARTESIAN_POINT ( 'NONE',  ( 13.50000000000000355, -1.317096457811611332, -13.00000000000000000 ) ) ;
#60528=ORIENTED_EDGE ( 'NONE', *, *, #22963, .F. ) ;
#60659=B_SPLINE_CURVE_WITH_KNOTS ( 'NONE', 3,
 ( #48442, #81333, #40359, #73238, #99659, #67312, #60300, #42483 ),
 .UNSPECIFIED., .F., .F.,
 ( 4, 2, 2, 4 ),
 ( 0.007886720825438852528, 0.009850969036564046280, 0.01181521724768924003, 0.01574371366993963101 ),
 .UNSPECIFIED. ) ;
#60873=VERTEX_POINT ( 'NONE', #90016 ) ;
#60891=ORIENTED_EDGE ( 'NONE', *, *, #34766, .F. ) ;
#60946=CIRCLE ( 'NONE', #74696, 8.000000000000000000 ) ;
#61211=ORIENTED_EDGE ( 'NONE', *, *, #18230, .T. ) ;
#61287=ORIENTED_EDGE ( 'NONE', *, *, #42155, .T. ) ;
#61321=CARTESIAN_POINT ( 'NONE',  ( -8.000000000000000000, 0.000000000000000000, -3.725171428571429022 ) ) ;
#61371=ORIENTED_EDGE ( 'NONE', *, *, #12871, .T. ) ;
#61377=CARTESIAN_POINT ( 'NONE',  ( -13.50000000000000000, 3.304540750553650152, -0.2220019300505651771 ) ) ;
#61511=AXIS2_PLACEMENT_3D ( 'NONE', #95660, #78406, #5575 ) ;
#61552=CARTESIAN_POINT ( 'NONE',  ( 13.50000000000000533, -7.794228634059982674, -11.79422863405993382 ) ) ;
#61601=B_SPLINE_CURVE_WITH_KNOTS ( 'NONE', 3,
 ( #58198, #67891, #9105, #75978, #34505, #83531, #67370, #2075 ),
 .UNSPECIFIED., .F., .F.,
 ( 4, 2, 2, 4 ),
 ( 0.007886720825438852528, 0.009850969036564048015, 0.01181521724768924524, 0.01574371366993963101 ),
 .UNSPECIFIED. ) ;
#61687=CARTESIAN_POINT ( 'NONE',  ( -8.000000000000000000, 0.000000000000000000, -7.424942857142857733 ) ) ;
#61716=CARTESIAN_POINT ( 'NONE',  ( 2.212097561415784952, -14.31130214556283065, -12.46447053051439724 ) ) ;
#61790=CIRCLE ( 'NONE', #25859, 7.000000000000000000 ) ;
#61969=CIRCLE ( 'NONE', #18866, 7.000000000000000000 ) ;
#61971=FACE_OUTER_BOUND ( 'NONE', #93199, .T. ) ;
#61982=ORIENTED_EDGE ( 'NONE', *, *, #8406, .T. ) ;
#61995=EDGE_CURVE ( 'NONE', #70854, #32906, #93773, .T. ) ;
#62114=CARTESIAN_POINT ( 'NONE',  ( -13.50000000000000178, -5.228219631169437775, -12.46710323223871164 ) ) ;
#62333=CARTESIAN_POINT ( 'NONE',  ( 6.750000000000017764, 11.69134295108991317, -13.00000000000000000 ) ) ;
#62390=CARTESIAN_POINT ( 'NONE',  ( 0.000000000000000000, 0.000000000000000000, 0.000000000000000000 ) ) ;
#62484=CARTESIAN_POINT ( 'NONE',  ( -3.601501433546143538E-16, 15.58845726811991206, -13.00000000000000000 ) ) ;
#62493=DIRECTION ( 'NONE',  ( -0.000000000000000000, -0.000000000000000000, -1.000000000000000000 ) ) ;
#62509=VECTOR ( 'NONE', #5704, 999.9999999999998863 ) ;
#62511=EDGE_CURVE ( 'NONE', #50065, #30636, #40396, .T. ) ;
#62522=DIRECTION ( 'NONE',  ( -0.000000000000000000, -0.000000000000000000, -1.000000000000000000 ) ) ;
#62646=ORIENTED_EDGE ( 'NONE', *, *, #100665, .F. ) ;
#62683=CARTESIAN_POINT ( 'NONE',  ( 0.000000000000000000, 0.000000000000000000, -8.125150395352576993 ) ) ;
#62713=ORIENTED_EDGE ( 'NONE', *, *, #1262, .F. ) ;
#62839=CARTESIAN_POINT ( 'NONE',  ( -2.216488688100143101, -14.30876692738956812, -12.46553453015538793 ) ) ;
#62983=DIRECTION ( 'NONE',  ( -0.000000000000000000, -0.000000000000000000, -1.000000000000000000 ) ) ;
#63059=CARTESIAN_POINT ( 'NONE',  ( -6.177150199754209758, 12.02207793746705455, -13.00000000000000888 ) ) ;
#63208=DIRECTION ( 'NONE',  ( 0.000000000000000000, 0.000000000000000000, 1.000000000000000000 ) ) ;
#63302=VECTOR ( 'NONE', #49705, 1000.000000000000000 ) ;
#63342=FACE_OUTER_BOUND ( 'NONE', #24555, .T. ) ;
#63384=AXIS2_PLACEMENT_3D ( 'NONE', #65520, #14828, #89800 ) ;
#63488=DIRECTION ( 'NONE',  ( 1.000000000000000000, 0.000000000000000000, 0.000000000000000000 ) ) ;
#63694=EDGE_CURVE ( 'NONE', #56403, #67861, #67038, .T. ) ;
#63697=CARTESIAN_POINT ( 'NONE',  ( -13.49999999999999822, -6.526560492696113158, -12.16017290538970563 ) ) ;
#63853=VECTOR ( 'NONE', #87884, 999.9999999999998863 ) ;
#63856=EDGE_CURVE ( 'NONE', #7125, #56853, #93678, .T. ) ;
#63913=ORIENTED_EDGE ( 'NONE', *, *, #79768, .F. ) ;
#63962=ORIENTED_EDGE ( 'NONE', *, *, #27185, .T. ) ;
#64061=ORIENTED_EDGE ( 'NONE', *, *, #79789, .T. ) ;
#64277=DIRECTION ( 'NONE',  ( 0.000000000000000000, 0.000000000000000000, 1.000000000000000000 ) ) ;
#64283=ORIENTED_EDGE ( 'NONE', *, *, #41470, .T. ) ;
#64330=EDGE_CURVE ( 'NONE', #30181, #21224, #104448, .T. ) ;
#64389=ORIENTED_EDGE ( 'NONE', *, *, #10849, .F. ) ;
#64398=VERTEX_POINT ( 'NONE', #22493 ) ;
#64473=DIRECTION ( 'NONE',  ( 1.000000000000000000, 0.000000000000000000, 0.000000000000000000 ) ) ;
#64475=VERTEX_POINT ( 'NONE', #47766 ) ;
#64513=VERTEX_POINT ( 'NONE', #23009 ) ;
#64540=DIRECTION ( 'NONE',  ( 0.000000000000000000, 0.000000000000000000, 1.000000000000000000 ) ) ;
#64656=ORIENTED_EDGE ( 'NONE', *, *, #34598, .T. ) ;
#64660=CARTESIAN_POINT ( 'NONE',  ( 0.000000000000000000, 0.000000000000000000, -8.574621033218877031 ) ) ;
#64727=LINE ( 'NONE', #6472, #102728 ) ;
#64759=DIRECTION ( 'NONE',  ( -1.000000000000000000, 0.000000000000000000, 0.000000000000000000 ) ) ;
#64783=PLANE ( 'NONE',  #15118 ) ;
#64799=LINE ( 'NONE', #106300, #99141 ) ;
#64843=ORIENTED_EDGE ( 'NONE', *, *, #47428, .T. ) ;
#64849=CARTESIAN_POINT ( 'NONE',  ( 0.000000000000000000, 0.000000000000000000, 0.000000000000000000 ) ) ;
#64973=AXIS2_PLACEMENT_3D ( 'NONE', #92367, #58964, #2284 ) ;
#65038=ADVANCED_FACE ( 'NONE', ( #73509 ), #83572, .T. ) ;
#65100=VECTOR ( 'NONE', #101434, 1000.000000000000227 ) ;
#65275=COLOUR_RGB ( '', 0.09019608, 0.27058824, 0.51372549) ;
#65276=AXIS2_PLACEMENT_3D ( 'NONE', #62390, #35072, #94766 ) ;
#65312=DIRECTION ( 'NONE',  ( -1.000000000000000000, 0.000000000000000000, 0.000000000000000000 ) ) ;
#65313=DIRECTION ( 'NONE',  ( 0.8191520442889974607, 1.003171929053531649E-16, -0.5735764363510380548 ) ) ;
#65376=CARTESIAN_POINT ( 'NONE',  ( 0.000000000000000000, 0.000000000000000000, -1.875285714285714445 ) ) ;
#65438=ORIENTED_EDGE ( 'NONE', *, *, #6513, .F. ) ;
#65439=DIRECTION ( 'NONE',  ( 0.000000000000000000, 0.000000000000000000, -1.000000000000000000 ) ) ;
#65461=ORIENTED_EDGE ( 'NONE', *, *, #31341, .T. ) ;
#65520=CARTESIAN_POINT ( 'NONE',  ( 0.000000000000000000, 0.000000000000000000, -13.00000000000000000 ) ) ;
#65563=DIRECTION ( 'NONE',  ( -0.000000000000000000, -0.000000000000000000, -1.000000000000000000 ) ) ;
#65690=AXIS2_PLACEMENT_3D ( 'NONE', #81471, #50190, #6 ) ;
#65778=DIRECTION ( 'NONE',  ( -1.000000000000000000, 0.000000000000000000, 0.000000000000000000 ) ) ;
#65814=DIRECTION ( 'NONE',  ( -1.000000000000000000, 0.000000000000000000, 0.000000000000000000 ) ) ;
#65859=ORIENTED_EDGE ( 'NONE', *, *, #10204, .T. ) ;
#65878=ORIENTED_EDGE ( 'NONE', *, *, #77865, .T. ) ;
#65922=EDGE_CURVE ( 'NONE', #21504, #23394, #66733, .T. ) ;
#66003=ORIENTED_EDGE ( 'NONE', *, *, #11431, .T. ) ;
#66116=ORIENTED_EDGE ( 'NONE', *, *, #2098, .F. ) ;
#66201=DIRECTION ( 'NONE',  ( 1.000000000000000000, 0.000000000000000000, 0.000000000000000000 ) ) ;
#66220=CARTESIAN_POINT ( 'NONE',  ( 0.000000000000000000, 0.000000000000000000, -12.27439246179028309 ) ) ;
#66258=DIRECTION ( 'NONE',  ( -1.000000000000000000, 0.000000000000000000, 0.000000000000000000 ) ) ;
#66279=ORIENTED_EDGE ( 'NONE', *, *, #90808, .T. ) ;
#66286=EDGE_LOOP ( 'NONE', ( #68316, #54966, #64843, #18026 ) ) ;
#66635=ADVANCED_FACE ( 'NONE', ( #3999 ), #68356, .F. ) ;
#66692=EDGE_CURVE ( 'NONE', #64398, #47413, #1167, .T. ) ;
#66733=LINE ( 'NONE', #99617, #85530 ) ;
#66782=EDGE_CURVE ( 'NONE', #35268, #64398, #7157, .T. ) ;
#66821=DIRECTION ( 'NONE',  ( 0.000000000000000000, 0.000000000000000000, -1.000000000000000000 ) ) ;
#66840=AXIS2_PLACEMENT_3D ( 'NONE', #41960, #91593, #43037 ) ;
#66970=LINE ( 'NONE', #56174, #30586 ) ;
#67003=DIRECTION ( 'NONE',  ( 0.8191520442889884679, 0.000000000000000000, 0.5735764363510509334 ) ) ;
#67013=EDGE_LOOP ( 'NONE', ( #73572, #76066, #105094, #77827 ) ) ;
#67038=B_SPLINE_CURVE_WITH_KNOTS ( 'NONE', 3,
 ( #52133, #75340, #26325, #85051, #102289, #42451 ),
 .UNSPECIFIED., .F., .F.,
 ( 4, 2, 4 ),
 ( 2.380729204634966319E-07, 0.003943479449179620316, 0.007886720825438776200 ),
 .UNSPECIFIED. ) ;
#67198=ORIENTED_EDGE ( 'NONE', *, *, #10031, .T. ) ;
#67228=CIRCLE ( 'NONE', #15463, 7.000000000000000000 ) ;
#67253=CARTESIAN_POINT ( 'NONE',  ( -8.000000000000000000, 9.797174393178825657E-16, -13.00000000000000000 ) ) ;
#67293=APPLICATION_CONTEXT ( 'automotive_design' ) ;
#67303=CONICAL_SURFACE ( 'NONE', #19147, 8.000000000000000000, 0.9599310885968911355 ) ;
#67305=DIRECTION ( 'NONE',  ( -0.000000000000000000, -0.000000000000000000, 1.000000000000000000 ) ) ;
#67312=CARTESIAN_POINT ( 'NONE',  ( -11.28790243858421150, -9.071383756617100502, -0.5355294694855911031 ) ) ;
#67345=CARTESIAN_POINT ( 'NONE',  ( -13.50000000000000355, 3.304540750553675021, -12.77799806994943310 ) ) ;
#67369=CARTESIAN_POINT ( 'NONE',  ( 0.000000000000000000, 0.000000000000000000, -13.00000000000000000 ) ) ;
#67370=CARTESIAN_POINT ( 'NONE',  ( -12.39854599882999153, -8.430153398135473708, -12.16137996778341268 ) ) ;
#67437=VECTOR ( 'NONE', #52296, 999.9999999999998863 ) ;
#67516=FACE_OUTER_BOUND ( 'NONE', #47070, .T. ) ;
#67701=CARTESIAN_POINT ( 'NONE',  ( -7.000000000000000000, 8.572527594031473190E-16, -4.425378966781146950 ) ) ;
#67708=FACE_OUTER_BOUND ( 'NONE', #67013, .T. ) ;
#67861=VERTEX_POINT ( 'NONE', #36295 ) ;
#67865=CARTESIAN_POINT ( 'NONE',  ( -13.50000000000000533, 6.533945317241111717, -12.15804109017022405 ) ) ;
#67868=CARTESIAN_POINT ( 'NONE',  ( 0.000000000000000000, 0.000000000000000000, -11.82492182392400437 ) ) ;
#67891=CARTESIAN_POINT ( 'NONE',  ( -7.322849800245839980, -11.36060796471280376, -12.99999999999999467 ) ) ;
#67921=ADVANCED_BREP_SHAPE_REPRESENTATION ( '', ( #90584, #10728 ), #83338 ) ;
#67942=FACE_OUTER_BOUND ( 'NONE', #3210, .T. ) ;
#67991=ORIENTED_EDGE ( 'NONE', *, *, #63694, .T. ) ;
#68006=VERTEX_POINT ( 'NONE', #49631 ) ;
#68023=( LENGTH_UNIT ( ) NAMED_UNIT ( * ) SI_UNIT ( .MILLI., .METRE. ) );
#68063=ORIENTED_EDGE ( 'NONE', *, *, #57027, .F. ) ;
#68219=CIRCLE ( 'NONE', #2767, 8.000000000000000000 ) ;
#68316=ORIENTED_EDGE ( 'NONE', *, *, #50687, .F. ) ;
#68355=( NAMED_UNIT ( * ) SI_UNIT ( $, .STERADIAN. ) SOLID_ANGLE_UNIT ( ) );
#68356=CONICAL_SURFACE ( 'NONE', #59736, 8.000000000000000000, 0.9599310885968798113 ) ;
#68361=EDGE_CURVE ( 'NONE', #17308, #91520, #13508, .T. ) ;
#68464=DIRECTION ( 'NONE',  ( 0.000000000000000000, 0.000000000000000000, 1.000000000000000000 ) ) ;
#68486=ADVANCED_FACE ( 'NONE', ( #63342 ), #22175, .F. ) ;
#68504=FACE_OUTER_BOUND ( 'NONE', #3265, .T. ) ;
#68543=AXIS2_PLACEMENT_3D ( 'NONE', #15681, #48571, #76571 ) ;
#68613=EDGE_CURVE ( 'NONE', #102378, #20513, #47994, .T. ) ;
#68642=DIRECTION ( 'NONE',  ( 0.8660254037844380415, -0.5000000000000011102, 0.000000000000000000 ) ) ;
#68756=CARTESIAN_POINT ( 'NONE',  ( -7.000000000000000000, 8.572527594031471218E-16, -13.00000000000000000 ) ) ;
#68766=DIRECTION ( 'NONE',  ( -0.000000000000000000, -0.000000000000000000, -1.000000000000000000 ) ) ;
#69001=EDGE_CURVE ( 'NONE', #23867, #17408, #71791, .T. ) ;
#69028=EDGE_CURVE ( 'NONE', #79700, #33682, #104702, .T. ) ;
#69050=DIRECTION ( 'NONE',  ( -0.000000000000000000, -0.000000000000000000, 1.000000000000000000 ) ) ;
#69142=EDGE_CURVE ( 'NONE', #96238, #58987, #27426, .T. ) ;
#69173=AXIS2_PLACEMENT_3D ( 'NONE', #1991, #33333, #66201 ) ;
#69412=ORIENTED_EDGE ( 'NONE', *, *, #53828, .T. ) ;
#69573=CARTESIAN_POINT ( 'NONE',  ( 7.000000000000000000, 0.000000000000000000, -6.275264681066861527 ) ) ;
#69604=LINE ( 'NONE', #20032, #65100 ) ;
#69811=CYLINDRICAL_SURFACE ( 'NONE', #29361, 7.000000000000000000 ) ;
#69834=DIRECTION ( 'NONE',  ( -1.000000000000000000, 0.000000000000000000, 0.000000000000000000 ) ) ;
#69929=ORIENTED_EDGE ( 'NONE', *, *, #88311, .T. ) ;
#69939=ADVANCED_FACE ( 'NONE', ( #92517 ), #53139, .T. ) ;
#70023=CARTESIAN_POINT ( 'NONE',  ( -8.000000000000000000, 0.000000000000000000, -9.274828571428571422 ) ) ;
#70037=CARTESIAN_POINT ( 'NONE',  ( 6.750000000000017764, 11.69134295108991317, 0.000000000000000000 ) ) ;
#70135=CIRCLE ( 'NONE', #51172, 13.50000000000000000 ) ;
#70154=CARTESIAN_POINT ( 'NONE',  ( 13.50000000000000355, -6.526560492696113158, -12.16017290538970386 ) ) ;
#70243=ORIENTED_EDGE ( 'NONE', *, *, #45983, .T. ) ;
#70314=ORIENTED_EDGE ( 'NONE', *, *, #7938, .T. ) ;
#70390=AXIS2_PLACEMENT_3D ( 'NONE', #17108, #8988, #34380 ) ;
#70529=ORIENTED_EDGE ( 'NONE', *, *, #55082, .T. ) ;
#70571=DIRECTION ( 'NONE',  ( 1.000000000000000000, 0.000000000000000000, 0.000000000000000000 ) ) ;
#70603=DIRECTION ( 'NONE',  ( -1.000000000000000000, 0.000000000000000000, 0.000000000000000000 ) ) ;
#70731=EDGE_LOOP ( 'NONE', ( #100693, #71122, #56587, #56559, #33716, #102991 ) ) ;
#70803=CARTESIAN_POINT ( 'NONE',  ( 0.000000000000000000, 0.000000000000000000, -3.024963890361733743 ) ) ;
#70824=CARTESIAN_POINT ( 'NONE',  ( -8.000000000000000000, 0.000000000000000000, -5.575057142857143155 ) ) ;
#70854=VERTEX_POINT ( 'NONE', #73691 ) ;
#70862=VECTOR ( 'NONE', #55687, 1000.000000000000000 ) ;
#70970=CARTESIAN_POINT ( 'NONE',  ( 0.000000000000000000, 0.000000000000000000, -11.82492182392400437 ) ) ;
#70978=CARTESIAN_POINT ( 'NONE',  ( 7.000000000000000000, 0.000000000000000000, -0.7256075382097185722 ) ) ;
#71038=CONICAL_SURFACE ( 'NONE', #79658, 8.000000000000000000, 0.9599310885968911355 ) ;
#71087=DIRECTION ( 'NONE',  ( 0.000000000000000000, 0.000000000000000000, 1.000000000000000000 ) ) ;
#71100=B_SPLINE_CURVE_WITH_KNOTS ( 'NONE', 3,
 ( #50474, #52081, #1382, #92543, #3005, #10556 ),
 .UNSPECIFIED., .F., .F.,
 ( 4, 2, 4 ),
 ( 2.380729204837650980E-07, 0.003943479449179637664, 0.007886720825438791813 ),
 .UNSPECIFIED. ) ;
#71122=ORIENTED_EDGE ( 'NONE', *, *, #18993, .F. ) ;
#71156=ORIENTED_EDGE ( 'NONE', *, *, #47428, .F. ) ;
#71525=EDGE_CURVE ( 'NONE', #7125, #14406, #94685, .T. ) ;
#71544=EDGE_CURVE ( 'NONE', #91520, #17308, #61969, .T. ) ;
#71600=EDGE_CURVE ( 'NONE', #99841, #91137, #90166, .T. ) ;
#71611=ORIENTED_EDGE ( 'NONE', *, *, #80372, .F. ) ;
#71627=VERTEX_POINT ( 'NONE', #23330 ) ;
#71678=LINE ( 'NONE', #20015, #102555 ) ;
#71732=CARTESIAN_POINT ( 'NONE',  ( 13.50000000000000355, -2.625659737069745869, -0.1132121849006624686 ) ) ;
#71741=AXIS2_PLACEMENT_3D ( 'NONE', #45198, #96913, #53275 ) ;
#71791=LINE ( 'NONE', #28740, #84273 ) ;
#71802=CARTESIAN_POINT ( 'NONE',  ( 6.750000000000017764, 11.69134295108991317, 0.000000000000000000 ) ) ;
#71849=CONICAL_SURFACE ( 'NONE', #59787, 8.000000000000000000, 0.9599310885968911355 ) ;
#71961=VERTEX_POINT ( 'NONE', #34898 ) ;
#72096=DIRECTION ( 'NONE',  ( -1.000000000000000000, 0.000000000000000000, 0.000000000000000000 ) ) ;
#72124=CARTESIAN_POINT ( 'NONE',  ( 13.50000000000000355, 7.794228634059934713, -13.00000000000000000 ) ) ;
#72142=ORIENTED_EDGE ( 'NONE', *, *, #59427, .T. ) ;
#72168=ORIENTED_EDGE ( 'NONE', *, *, #43077, .T. ) ;
#72174=AXIS2_PLACEMENT_3D ( 'NONE', #50795, #1166, #57827 ) ;
#72208=EDGE_CURVE ( 'NONE', #58987, #102378, #91908, .T. ) ;
#72282=DIRECTION ( 'NONE',  ( -0.8191520442889974607, 0.000000000000000000, -0.5735764363510380548 ) ) ;
#72292=CARTESIAN_POINT ( 'NONE',  ( -13.50000000000000000, -2.625659737069751198, -12.88678781509933735 ) ) ;
#72317=CARTESIAN_POINT ( 'NONE',  ( 0.000000000000000000, 0.000000000000000000, -0.7702282920306786629 ) ) ;
#72322=VECTOR ( 'NONE', #105359, 1000.000000000000000 ) ;
#72355=ORIENTED_EDGE ( 'NONE', *, *, #3372, .T. ) ;
#72382=CARTESIAN_POINT ( 'NONE',  ( 1.101454001169993813, -14.95253250404446277, -0.8386200322166146304 ) ) ;
#72603=CIRCLE ( 'NONE', #69173, 13.50000000000000178 ) ;
#72682=CARTESIAN_POINT ( 'NONE',  ( 7.000000000000000000, 0.000000000000000000, -11.82492182392400437 ) ) ;
#72892=CARTESIAN_POINT ( 'NONE',  ( 0.000000000000000000, 0.000000000000000000, 3.469446951953614189E-15 ) ) ;
#72902=AXIS2_PLACEMENT_3D ( 'NONE', #27856, #53668, #86070 ) ;
#72919=DIRECTION ( 'NONE',  ( -1.000000000000000000, 0.000000000000000000, 0.000000000000000000 ) ) ;
#72953=ORIENTED_EDGE ( 'NONE', *, *, #18230, .F. ) ;
#72961=EDGE_LOOP ( 'NONE', ( #33969, #62646, #37993 ) ) ;
#73072=AXIS2_PLACEMENT_3D ( 'NONE', #77633, #62522, #3753 ) ;
#73088=CARTESIAN_POINT ( 'NONE',  ( 13.50000000000000355, 0.6589394956329810427, -9.910285482875310023E-16 ) ) ;
#73134=DIRECTION ( 'NONE',  ( -1.000000000000000000, 0.000000000000000000, 0.000000000000000000 ) ) ;
#73184=DIRECTION ( 'NONE',  ( 0.000000000000000000, 0.000000000000000000, 1.000000000000000000 ) ) ;
#73211=FACE_OUTER_BOUND ( 'NONE', #66286, .T. ) ;
#73222=DIRECTION ( 'NONE',  ( 0.000000000000000000, 0.000000000000000000, 1.000000000000000000 ) ) ;
#73238=CARTESIAN_POINT ( 'NONE',  ( -9.036570576874968452, -10.37119081301011647, -0.1387913946425914369 ) ) ;
#73271=AXIS2_PLACEMENT_3D ( 'NONE', #11125, #43522, #85589 ) ;
#73345=AXIS2_PLACEMENT_3D ( 'NONE', #46934, #23224, #30251 ) ;
#73425=DIRECTION ( 'NONE',  ( 1.000000000000000000, 0.000000000000000000, 0.000000000000000000 ) ) ;
#73464=ORIENTED_EDGE ( 'NONE', *, *, #43829, .F. ) ;
#73509=FACE_OUTER_BOUND ( 'NONE', #72961, .T. ) ;
#73572=ORIENTED_EDGE ( 'NONE', *, *, #17507, .F. ) ;
#73590=FACE_OUTER_BOUND ( 'NONE', #564, .T. ) ;
#73691=CARTESIAN_POINT ( 'NONE',  ( -8.000000000000000000, 0.000000000000000000, -1.875285714285714445 ) ) ;
#73753=CONICAL_SURFACE ( 'NONE', #8310, 7.000000000000000000, 0.9599310885968753704 ) ;
#73794=CARTESIAN_POINT ( 'NONE',  ( -4.463429423125060858, 13.01149508916975428, -0.1387913946425749778 ) ) ;
#73797=EDGE_LOOP ( 'NONE', ( #27035, #2118, #101567, #99985 ) ) ;
#73807=ORIENTED_EDGE ( 'NONE', *, *, #34598, .F. ) ;
#73910=ORIENTED_EDGE ( 'NONE', *, *, #36375, .F. ) ;
#74036=VECTOR ( 'NONE', #59482, 1000.000000000000000 ) ;
#74104=CIRCLE ( 'NONE', #27670, 7.000000000000000000 ) ;
#74189=VERTEX_POINT ( 'NONE', #74689 ) ;
#74199=B_SPLINE_CURVE_WITH_KNOTS ( 'NONE', 3,
 ( #93205, #52201, #83504, #74867, #67345, #34478, #67865, #9606 ),
 .UNSPECIFIED., .F., .F.,
 ( 4, 2, 2, 4 ),
 ( 0.02179091314793462145, 0.02376333058066962614, 0.02573574801340463430, 0.02968058287887464369 ),
 .UNSPECIFIED. ) ;
#74231=DIRECTION ( 'NONE',  ( -0.000000000000000000, 0.000000000000000000, -1.000000000000000000 ) ) ;
#74292=SHAPE_REPRESENTATION ( 'hex nut high strength_din_Hexagon Nut DIN 6915 - M16 - S', ( #10728 ), #83338 ) ;
#74337=EDGE_LOOP ( 'NONE', ( #104497, #36346, #52306, #59034 ) ) ;
#74344=ORIENTED_EDGE ( 'NONE', *, *, #23528, .T. ) ;
#74474=DIRECTION ( 'NONE',  ( -0.000000000000000000, -0.000000000000000000, 1.000000000000000000 ) ) ;
#74478=CONICAL_SURFACE ( 'NONE', #3837, 7.000000000000000000, 0.9599310885968753704 ) ;
#74502=CARTESIAN_POINT ( 'NONE',  ( -7.000000000000000000, 8.572527594031471218E-16, -13.00000000000000000 ) ) ;
#74689=CARTESIAN_POINT ( 'NONE',  ( 8.000000000000000000, 9.797174393178825657E-16, -5.575057142857143155 ) ) ;
#74696=AXIS2_PLACEMENT_3D ( 'NONE', #83319, #8894, #16460 ) ;
#74699=CARTESIAN_POINT ( 'NONE',  ( -7.000000000000000000, 8.572527594031471218E-16, -6.275264681066861527 ) ) ;
#74732=CARTESIAN_POINT ( 'NONE',  ( 0.000000000000000000, 0.000000000000000000, -13.00000000000000000 ) ) ;
#74784=CIRCLE ( 'NONE', #7634, 8.000000000000000000 ) ;
#74867=CARTESIAN_POINT ( 'NONE',  ( -13.50000000000000178, 2.646256834279085979, -12.86070865178833600 ) ) ;
#74998=DIRECTION ( 'NONE',  ( 1.000000000000000000, 0.000000000000000000, 0.000000000000000000 ) ) ;
#75160=CARTESIAN_POINT ( 'NONE',  ( 13.50000000000000355, 7.794228634059978233, -11.79422863405993382 ) ) ;
#75170=CARTESIAN_POINT ( 'NONE',  ( 0.000000000000000000, 0.000000000000000000, -2.575493252495433261 ) ) ;
#75182=CARTESIAN_POINT ( 'NONE',  ( -7.000000000000000000, 8.572527594031471218E-16, -0.7256075382097185722 ) ) ;
#75275=CONICAL_SURFACE ( 'NONE', #78736, 7.000000000000000000, 0.9599310885968753704 ) ;
#75313=B_SPLINE_CURVE_WITH_KNOTS ( 'NONE', 3,
 ( #76644, #3299, #4358, #11912, #44840, #27619, #86370, #59969 ),
 .UNSPECIFIED., .F., .F.,
 ( 4, 2, 2, 4 ),
 ( 0.007886720825438833446, 0.009850969036564030668, 0.01181521724768922615, 0.01574371366993962407 ),
 .UNSPECIFIED. ) ;
#75333=EDGE_LOOP ( 'NONE', ( #33290, #89274, #21596, #53277 ) ) ;
#75339=ORIENTED_EDGE ( 'NONE', *, *, #26371, .T. ) ;
#75340=CARTESIAN_POINT ( 'NONE',  ( 12.39578842395471270, -8.431745484732026341, -12.16229915940863293 ) ) ;
#75378=DIRECTION ( 'NONE',  ( -1.000000000000000000, 0.000000000000000000, 0.000000000000000000 ) ) ;
#75456=ORIENTED_EDGE ( 'NONE', *, *, #68361, .F. ) ;
#75492=CARTESIAN_POINT ( 'NONE',  ( 0.000000000000000000, 0.000000000000000000, -9.274828571428571422 ) ) ;
#75508=EDGE_CURVE ( 'NONE', #91137, #47413, #23420, .T. ) ;
#75521=AXIS2_PLACEMENT_3D ( 'NONE', #17318, #50193, #83095 ) ;
#75571=CARTESIAN_POINT ( 'NONE',  ( -4.464296094009080562, -13.01099471650159600, -0.1149164202474959318 ) ) ;
#75592=DIRECTION ( 'NONE',  ( 1.000000000000000000, 0.000000000000000000, 0.000000000000000000 ) ) ;
#75733=ORIENTED_EDGE ( 'NONE', *, *, #62511, .F. ) ;
#75801=CARTESIAN_POINT ( 'NONE',  ( 7.000000000000000000, 0.000000000000000000, -6.724735318933162453 ) ) ;
#75951=ADVANCED_FACE ( 'NONE', ( #48579, #96626 ), #64783, .F. ) ;
#75967=FACE_BOUND ( 'NONE', #59075, .T. ) ;
#75978=CARTESIAN_POINT ( 'NONE',  ( -9.036570576874968452, -10.37119081301011292, -12.86120860535740640 ) ) ;
#76066=ORIENTED_EDGE ( 'NONE', *, *, #79397, .T. ) ;
#76125=CARTESIAN_POINT ( 'NONE',  ( 13.50000000000000178, 0.000000000000000000, -13.00000000000000000 ) ) ;
#76154=DIRECTION ( 'NONE',  ( 1.000000000000000000, 0.000000000000000000, 0.000000000000000000 ) ) ;
#76167=CARTESIAN_POINT ( 'NONE',  ( 7.000000000000000000, 0.000000000000000000, -12.27439246179028309 ) ) ;
#76283=FACE_OUTER_BOUND ( 'NONE', #88090, .T. ) ;
#76304=LINE ( 'NONE', #67701, #48033 ) ;
#76330=CARTESIAN_POINT ( 'NONE',  ( 2.235495008889195345E-15, -15.58845726811994759, -13.00000000000000000 ) ) ;
#76334=DIRECTION ( 'NONE',  ( -0.000000000000000000, -0.000000000000000000, 1.000000000000000000 ) ) ;
#76388=DIRECTION ( 'NONE',  ( -1.000000000000000000, 0.000000000000000000, 0.000000000000000000 ) ) ;
#76533=CARTESIAN_POINT ( 'NONE',  ( 0.000000000000000000, 0.000000000000000000, -13.00000000000000000 ) ) ;
#76541=EDGE_CURVE ( 'NONE', #104233, #58364, #80785, .T. ) ;
#76571=DIRECTION ( 'NONE',  ( -1.000000000000000000, 0.000000000000000000, 0.000000000000000000 ) ) ;
#76609=DIRECTION ( 'NONE',  ( 0.000000000000000000, -0.000000000000000000, 1.000000000000000000 ) ) ;
#76639=FACE_OUTER_BOUND ( 'NONE', #27819, .T. ) ;
#76644=CARTESIAN_POINT ( 'NONE',  ( 6.750000000000017764, 11.69134295108991317, 0.000000000000000000 ) ) ;
#76718=CARTESIAN_POINT ( 'NONE',  ( 0.000000000000000000, 0.000000000000000000, -9.975036109638290682 ) ) ;
#76895=DIRECTION ( 'NONE',  ( -1.000000000000000000, 0.000000000000000000, 0.000000000000000000 ) ) ;
#76911=CIRCLE ( 'NONE', #33904, 13.50000000000000000 ) ;
#77039=ORIENTED_EDGE ( 'NONE', *, *, #68361, .T. ) ;
#77162=AXIS2_PLACEMENT_3D ( 'NONE', #83789, #1252, #91892 ) ;
#77372=FACE_OUTER_BOUND ( 'NONE', #10929, .T. ) ;
#77489=ADVANCED_FACE ( 'NONE', ( #1317 ), #34410, .F. ) ;
#77498=DIRECTION ( 'NONE',  ( 0.000000000000000000, 0.000000000000000000, 1.000000000000000000 ) ) ;
#77616=DIRECTION ( 'NONE',  ( -1.000000000000000000, 0.000000000000000000, 0.000000000000000000 ) ) ;
#77633=CARTESIAN_POINT ( 'NONE',  ( 0.000000000000000000, 0.000000000000000000, -9.274828571428571422 ) ) ;
#77666=CARTESIAN_POINT ( 'NONE',  ( 0.000000000000000000, 0.000000000000000000, -25.03750572909317285 ) ) ;
#77670=CARTESIAN_POINT ( 'NONE',  ( -7.000000000000000000, 8.572527594031473190E-16, -6.275264681066861527 ) ) ;
#77728=EDGE_CURVE ( 'NONE', #64513, #34348, #10335, .T. ) ;
#77747=EDGE_LOOP ( 'NONE', ( #92069, #4727, #61371, #66279 ) ) ;
#77795=LINE ( 'NONE', #45435, #40261 ) ;
#77827=ORIENTED_EDGE ( 'NONE', *, *, #63856, .F. ) ;
#77865=EDGE_CURVE ( 'NONE', #2886, #70854, #23398, .T. ) ;
#77916=CARTESIAN_POINT ( 'NONE',  ( 0.000000000000000000, 0.000000000000000000, -1.875285714285714445 ) ) ;
#78070=AXIS2_PLACEMENT_3D ( 'NONE', #72124, #105034, #6309 ) ;
#78074=CONICAL_SURFACE ( 'NONE', #95327, 8.000000000000000000, 0.9599310885968911355 ) ;
#78130=DIRECTION ( 'NONE',  ( -1.000000000000000000, 0.000000000000000000, 0.000000000000000000 ) ) ;
#78146=ORIENTED_EDGE ( 'NONE', *, *, #66782, .T. ) ;
#78181=STYLED_ITEM ( 'NONE', ( #81986 ), #67921 ) ;
#78199=ORIENTED_EDGE ( 'NONE', *, *, #38184, .F. ) ;
#78331=CARTESIAN_POINT ( 'NONE',  ( 7.000000000000000000, 0.000000000000000000, -11.82492182392400437 ) ) ;
#78377=VECTOR ( 'NONE', #17330, 1000.000000000000000 ) ;
#78406=DIRECTION ( 'NONE',  ( -0.000000000000000000, -0.000000000000000000, -1.000000000000000000 ) ) ;
#78527=LINE ( 'NONE', #12200, #62509 ) ;
#78593=ORIENTED_EDGE ( 'NONE', *, *, #69142, .T. ) ;
#78668=ORIENTED_EDGE ( 'NONE', *, *, #27166, .F. ) ;
#78687=CARTESIAN_POINT ( 'NONE',  ( -5.601730134768053482, 12.35429686688392970, -12.97150009825810280 ) ) ;
#78698=ORIENTED_EDGE ( 'NONE', *, *, #15436, .F. ) ;
#78706=ORIENTED_EDGE ( 'NONE', *, *, #80372, .T. ) ;
#78707=CARTESIAN_POINT ( 'NONE',  ( 8.000000000000000000, 9.797174393178825657E-16, -11.12471428571428689 ) ) ;
#78715=CARTESIAN_POINT ( 'NONE',  ( 0.000000000000000000, 0.000000000000000000, -3.725171428571429022 ) ) ;
#78736=AXIS2_PLACEMENT_3D ( 'NONE', #36545, #77498, #96206 ) ;
#78939=ORIENTED_EDGE ( 'NONE', *, *, #68613, .F. ) ;
#78978=DIRECTION ( 'NONE',  ( -0.000000000000000000, -0.000000000000000000, -1.000000000000000000 ) ) ;
#78993=AXIS2_PLACEMENT_3D ( 'NONE', #48056, #64277, #81474 ) ;
#79082=FACE_OUTER_BOUND ( 'NONE', #21, .T. ) ;
#79110=EDGE_CURVE ( 'NONE', #15319, #42431, #10488, .T. ) ;
#79129=ADVANCED_FACE ( 'NONE', ( #67708 ), #41438, .F. ) ;
#79196=CARTESIAN_POINT ( 'NONE',  ( 0.000000000000000000, 0.000000000000000000, -9.975036109638290682 ) ) ;
#79397=EDGE_CURVE ( 'NONE', #14406, #71627, #25414, .T. ) ;
#79417=CARTESIAN_POINT ( 'NONE',  ( -5.724587470723463412E-14, -15.58845726811991561, -1.205771365940065953 ) ) ;
#79434=EDGE_LOOP ( 'NONE', ( #29054, #34261, #53818 ) ) ;
#79478=VECTOR ( 'NONE', #29489, 1000.000000000000000 ) ;
#79494=EDGE_LOOP ( 'NONE', ( #97631, #83500, #98013 ) ) ;
#79580=EDGE_LOOP ( 'NONE', ( #49540, #61982, #53074, #64389 ) ) ;
#79592=VERTEX_POINT ( 'NONE', #69573 ) ;
#79658=AXIS2_PLACEMENT_3D ( 'NONE', #42840, #18596, #41774 ) ;
#79700=VERTEX_POINT ( 'NONE', #47915 ) ;
#79730=ORIENTED_EDGE ( 'NONE', *, *, #71600, .F. ) ;
#79768=EDGE_CURVE ( 'NONE', #3475, #30636, #33369, .T. ) ;
#79789=EDGE_CURVE ( 'NONE', #58364, #84222, #35517, .T. ) ;
#79803=DIRECTION ( 'NONE',  ( 0.000000000000000000, 0.000000000000000000, -1.000000000000000000 ) ) ;
#79887=CARTESIAN_POINT ( 'NONE',  ( -13.50000000000000000, -7.794228634059976457, -13.00000000000000000 ) ) ;
#80020=DIRECTION ( 'NONE',  ( -0.000000000000000000, -0.000000000000000000, -1.000000000000000000 ) ) ;
#80092=EDGE_CURVE ( 'NONE', #96238, #20513, #13307, .T. ) ;
#80351=EDGE_LOOP ( 'NONE', ( #7931, #89213, #7473 ) ) ;
#80372=EDGE_CURVE ( 'NONE', #100438, #31665, #9672, .T. ) ;
#80375=EDGE_CURVE ( 'NONE', #3854, #64475, #27632, .T. ) ;
#80417=DIRECTION ( 'NONE',  ( -1.000000000000000000, 0.000000000000000000, 0.000000000000000000 ) ) ;
#80420=ORIENTED_EDGE ( 'NONE', *, *, #80375, .F. ) ;
#80437=AXIS2_PLACEMENT_3D ( 'NONE', #76718, #35786, #58968 ) ;
#80450=ORIENTED_EDGE ( 'NONE', *, *, #11431, .F. ) ;
#80457=ORIENTED_EDGE ( 'NONE', *, *, #51918, .T. ) ;
#80552=DIRECTION ( 'NONE',  ( 0.000000000000000000, 0.000000000000000000, 1.000000000000000000 ) ) ;
#80554=EDGE_CURVE ( 'NONE', #105782, #64513, #20885, .T. ) ;
#80572=CIRCLE ( 'NONE', #106440, 8.000000000000000000 ) ;
#80760=DIRECTION ( 'NONE',  ( -1.000000000000000000, 0.000000000000000000, 0.000000000000000000 ) ) ;
#80785=CIRCLE ( 'NONE', #72174, 13.50000000000000000 ) ;
#80827=AXIS2_PLACEMENT_3D ( 'NONE', #289, #6823, #73134 ) ;
#80854=DIRECTION ( 'NONE',  ( -0.000000000000000000, -0.000000000000000000, 1.000000000000000000 ) ) ;
#80885=CIRCLE ( 'NONE', #82586, 8.000000000000000000 ) ;
#80893=DIRECTION ( 'NONE',  ( -0.000000000000000000, -0.000000000000000000, -1.000000000000000000 ) ) ;
#81127=CARTESIAN_POINT ( 'NONE',  ( 0.000000000000000000, 0.000000000000000000, -0.7256075382097185722 ) ) ;
#81194=CARTESIAN_POINT ( 'NONE',  ( 13.50000000000000355, 7.794228634059978233, -1.205771365940065953 ) ) ;
#81301=DIRECTION ( 'NONE',  ( 1.000000000000000000, 0.000000000000000000, 0.000000000000000000 ) ) ;
#81333=CARTESIAN_POINT ( 'NONE',  ( -7.322849800245838203, -11.36060796471280376, -1.080221117633409222E-14 ) ) ;
#81344=CARTESIAN_POINT ( 'NONE',  ( -3.898086217683921717, 13.33789614101572596, -0.2204769333330995063 ) ) ;
#81393=DIRECTION ( 'NONE',  ( -0.000000000000000000, -0.000000000000000000, -1.000000000000000000 ) ) ;
#81432=CARTESIAN_POINT ( 'NONE',  ( 7.000000000000000000, 0.000000000000000000, -10.42450674750459072 ) ) ;
#81434=LINE ( 'NONE', #90078, #14081 ) ;
#81471=CARTESIAN_POINT ( 'NONE',  ( 0.000000000000000000, 0.000000000000000000, -4.425378966781146950 ) ) ;
#81474=DIRECTION ( 'NONE',  ( 1.000000000000000000, 0.000000000000000000, 0.000000000000000000 ) ) ;
#81577=ORIENTED_EDGE ( 'NONE', *, *, #94451, .F. ) ;
#81799=CARTESIAN_POINT ( 'NONE',  ( 11.28351131189992174, -9.073918974790322167, -0.5344654698446129615 ) ) ;
#81968=CIRCLE ( 'NONE', #35522, 7.000000000000000000 ) ;
#81986=PRESENTATION_STYLE_ASSIGNMENT (( #16202 ) ) ;
#82149=EDGE_CURVE ( 'NONE', #33365, #6815, #72603, .T. ) ;
#82245=ORIENTED_EDGE ( 'NONE', *, *, #69001, .F. ) ;
#82289=FACE_OUTER_BOUND ( 'NONE', #49074, .T. ) ;
#82354=CARTESIAN_POINT ( 'NONE',  ( 6.750000000000016875, -11.69134295108991495, 0.000000000000000000 ) ) ;
#82455=VECTOR ( 'NONE', #53397, 1000.000000000000000 ) ;
#82586=AXIS2_PLACEMENT_3D ( 'NONE', #14332, #55839, #24594 ) ;
#82652=ADVANCED_FACE ( 'NONE', ( #18482 ), #82662, .F. ) ;
#82662=CYLINDRICAL_SURFACE ( 'NONE', #26234, 7.000000000000000000 ) ;
#82731=FACE_OUTER_BOUND ( 'NONE', #1786, .T. ) ;
#82967=ORIENTED_EDGE ( 'NONE', *, *, #79768, .T. ) ;
#82987=DIRECTION ( 'NONE',  ( -0.000000000000000000, -0.000000000000000000, 1.000000000000000000 ) ) ;
#82988=DIRECTION ( 'NONE',  ( -1.000000000000000000, 0.000000000000000000, 0.000000000000000000 ) ) ;
#83095=DIRECTION ( 'NONE',  ( -1.000000000000000000, 0.000000000000000000, 0.000000000000000000 ) ) ;
#83124=EDGE_LOOP ( 'NONE', ( #97583, #38115, #62713, #90886, #50132, #43679 ) ) ;
#83132=CARTESIAN_POINT ( 'NONE',  ( -6.750000000000015099, -11.69134295108991495, 0.000000000000000000 ) ) ;
#83139=CARTESIAN_POINT ( 'NONE',  ( 13.50000000000000533, 1.319989657865596744, -12.97199716660744961 ) ) ;
#83254=DIRECTION ( 'NONE',  ( -0.8191520442889884679, 1.003171929053520679E-16, 0.5735764363510509334 ) ) ;
#83319=CARTESIAN_POINT ( 'NONE',  ( 0.000000000000000000, 0.000000000000000000, -3.725171428571429022 ) ) ;
#83338=( GEOMETRIC_REPRESENTATION_CONTEXT ( 3 ) GLOBAL_UNCERTAINTY_ASSIGNED_CONTEXT ( ( #18702 ) ) GLOBAL_UNIT_ASSIGNED_CONTEXT ( ( #68023, #41016, #8105 ) ) REPRESENTATION_CONTEXT ( 'NONE', 'WORKASPACE' ) );
#83360=ORIENTED_EDGE ( 'NONE', *, *, #44908, .T. ) ;
#83409=DIRECTION ( 'NONE',  ( -1.000000000000000000, 0.000000000000000000, 0.000000000000000000 ) ) ;
#83500=ORIENTED_EDGE ( 'NONE', *, *, #76541, .T. ) ;
#83504=CARTESIAN_POINT ( 'NONE',  ( -13.49999999999999822, 1.319989657865599186, -12.97199716660744961 ) ) ;
#83528=AXIS2_PLACEMENT_3D ( 'NONE', #67369, #41482, #51155 ) ;
#83531=CARTESIAN_POINT ( 'NONE',  ( -11.28790243858421327, -9.071383756617098726, -12.46447053051440790 ) ) ;
#83572=CONICAL_SURFACE ( 'NONE', #37124, 13.50000000000000178, 1.047197551196596077 ) ;
#83787=CARTESIAN_POINT ( 'NONE',  ( 6.750000000000017764, 11.69134295108991317, -13.00000000000000000 ) ) ;
#83789=CARTESIAN_POINT ( 'NONE',  ( 0.000000000000000000, 0.000000000000000000, -13.00000000000000000 ) ) ;
#83790=ADVANCED_FACE ( 'NONE', ( #4021 ), #78074, .F. ) ;
#83810=ORIENTED_EDGE ( 'NONE', *, *, #45983, .F. ) ;
#83871=ORIENTED_EDGE ( 'NONE', *, *, #7144, .T. ) ;
#84051=DIRECTION ( 'NONE',  ( -0.000000000000000000, -0.000000000000000000, -1.000000000000000000 ) ) ;
#84064=DIRECTION ( 'NONE',  ( 0.8191520442889884679, 0.000000000000000000, 0.5735764363510509334 ) ) ;
#84177=ORIENTED_EDGE ( 'NONE', *, *, #38114, .T. ) ;
#84222=VERTEX_POINT ( 'NONE', #10263 ) ;
#84273=VECTOR ( 'NONE', #54012, 1000.000000000000000 ) ;
#84304=AXIS2_PLACEMENT_3D ( 'NONE', #31146, #96912, #72096 ) ;
#84351=ORIENTED_EDGE ( 'NONE', *, *, #56578, .F. ) ;
#84360=AXIS2_PLACEMENT_3D ( 'NONE', #76330, #102212, #93601 ) ;
#84505=DIRECTION ( 'NONE',  ( -1.000000000000000000, 0.000000000000000000, 0.000000000000000000 ) ) ;
#84508=CARTESIAN_POINT ( 'NONE',  ( -8.000000000000000000, 0.000000000000000000, -7.424942857142857733 ) ) ;
#84574=AXIS2_PLACEMENT_3D ( 'NONE', #50962, #17570, #50431 ) ;
#84585=ORIENTED_EDGE ( 'NONE', *, *, #38069, .F. ) ;
#84705=EDGE_LOOP ( 'NONE', ( #36328, #49038, #99938, #11660 ) ) ;
#84866=DIRECTION ( 'NONE',  ( 0.000000000000000000, 0.000000000000000000, 1.000000000000000000 ) ) ;
#84964=CARTESIAN_POINT ( 'NONE',  ( 8.000000000000000000, 0.000000000000000000, -13.00000000000000000 ) ) ;
#84988=ORIENTED_EDGE ( 'NONE', *, *, #90808, .F. ) ;
#85051=CARTESIAN_POINT ( 'NONE',  ( 9.035703905990985163, -10.37169118567828185, -12.88508357975250185 ) ) ;
#85128=LINE ( 'NONE', #35551, #16016 ) ;
#85192=VECTOR ( 'NONE', #44879, 1000.000000000000000 ) ;
#85211=EDGE_CURVE ( 'NONE', #24805, #6815, #28540, .T. ) ;
#85435=CARTESIAN_POINT ( 'NONE',  ( 3.898086217683916832, -13.33789614101576682, -12.77952306666688109 ) ) ;
#85507=CARTESIAN_POINT ( 'NONE',  ( 7.000000000000000000, 0.000000000000000000, -9.975036109638290682 ) ) ;
#85530=VECTOR ( 'NONE', #25795, 999.9999999999998863 ) ;
#85536=CARTESIAN_POINT ( 'NONE',  ( 13.50000000000000178, 0.000000000000000000, 0.000000000000000000 ) ) ;
#85578=DIRECTION ( 'NONE',  ( -0.000000000000000000, -0.000000000000000000, -1.000000000000000000 ) ) ;
#85589=DIRECTION ( 'NONE',  ( 1.000000000000000000, 0.000000000000000000, 0.000000000000000000 ) ) ;
#85711=CIRCLE ( 'NONE', #40947, 7.000000000000000000 ) ;
#85748=( NAMED_UNIT ( * ) SI_UNIT ( $, .STERADIAN. ) SOLID_ANGLE_UNIT ( ) );
#85856=ORIENTED_EDGE ( 'NONE', *, *, #51143, .T. ) ;
#85919=ORIENTED_EDGE ( 'NONE', *, *, #39934, .F. ) ;
#86002=ORIENTED_EDGE ( 'NONE', *, *, #4796, .F. ) ;
#86070=DIRECTION ( 'NONE',  ( -1.000000000000000000, 0.000000000000000000, 0.000000000000000000 ) ) ;
#86096=ORIENTED_EDGE ( 'NONE', *, *, #14700, .T. ) ;
#86114=CONICAL_SURFACE ( 'NONE', #39596, 13.50000000000000178, 1.047197551196596077 ) ;
#86115=ORIENTED_EDGE ( 'NONE', *, *, #355, .F. ) ;
#86124=ORIENTED_EDGE ( 'NONE', *, *, #100665, .T. ) ;
#86245=DIRECTION ( 'NONE',  ( -0.5000000000000014433, 0.8660254037844379305, 0.000000000000000000 ) ) ;
#86296=DIRECTION ( 'NONE',  ( 0.000000000000000000, 0.000000000000000000, 1.000000000000000000 ) ) ;
#86370=CARTESIAN_POINT ( 'NONE',  ( 12.39854599882998798, 8.430153398135439957, -0.8386200322165747734 ) ) ;
#86373=ORIENTED_EDGE ( 'NONE', *, *, #44750, .T. ) ;
#86386=ADVANCED_FACE ( 'NONE', ( #34504 ), #28458, .T. ) ;
#86460=VECTOR ( 'NONE', #24386, 1000.000000000000227 ) ;
#86584=VECTOR ( 'NONE', #106149, 1000.000000000000000 ) ;
#86686=CONICAL_SURFACE ( 'NONE', #95292, 8.000000000000000000, 0.9599310885968911355 ) ;
#86719=CARTESIAN_POINT ( 'NONE',  ( -13.50000000000000000, 7.794228634059933825, -1.205771365940051520 ) ) ;
#86770=CARTESIAN_POINT ( 'NONE',  ( 0.000000000000000000, 0.000000000000000000, -13.00000000000000000 ) ) ;
#86808=( LENGTH_UNIT ( ) NAMED_UNIT ( * ) SI_UNIT ( .MILLI., .METRE. ) );
#86905=ORIENTED_EDGE ( 'NONE', *, *, #34766, .T. ) ;
#86921=EDGE_CURVE ( 'NONE', #44907, #71961, #37153, .T. ) ;
#86934=CONICAL_SURFACE ( 'NONE', #90614, 7.000000000000000000, 0.9599310885968753704 ) ;
#86956=DIRECTION ( 'NONE',  ( 0.000000000000000000, 0.000000000000000000, 1.000000000000000000 ) ) ;
#87002=CARTESIAN_POINT ( 'NONE',  ( 3.898086217683919497, -13.33789614101576149, -0.2204769333331217940 ) ) ;
#87036=CONICAL_SURFACE ( 'NONE', #57722, 7.000000000000000000, 0.9599310885968753704 ) ;
#87061=EDGE_CURVE ( 'NONE', #92662, #21224, #105978, .T. ) ;
#87230=FACE_OUTER_BOUND ( 'NONE', #8238, .T. ) ;
#87489=CARTESIAN_POINT ( 'NONE',  ( 0.000000000000000000, 0.000000000000000000, -2.575493252495433261 ) ) ;
#87596=DIRECTION ( 'NONE',  ( 1.000000000000000000, 0.000000000000000000, 0.000000000000000000 ) ) ;
#87673=EDGE_CURVE ( 'NONE', #58987, #21224, #27698, .T. ) ;
#87681=FACE_OUTER_BOUND ( 'NONE', #100423, .T. ) ;
#87868=CARTESIAN_POINT ( 'NONE',  ( -4.463429423125057305, 13.01149508916975428, -12.86120860535742239 ) ) ;
#87870=AXIS2_PLACEMENT_3D ( 'NONE', #15099, #80893, #84505 ) ;
#87878=B_SPLINE_CURVE_WITH_KNOTS ( 'NONE', 3,
 ( #83787, #57382, #49830, #90295, #9899, #42807, #42267, #75160 ),
 .UNSPECIFIED., .F., .F.,
 ( 4, 2, 2, 4 ),
 ( 0.007886720825438833446, 0.009850969036564032402, 0.01181521724768922962, 0.01574371366993962754 ),
 .UNSPECIFIED. ) ;
#87884=DIRECTION ( 'NONE',  ( -0.8191520442889884679, 1.003171929053520679E-16, 0.5735764363510509334 ) ) ;
#87909=FACE_OUTER_BOUND ( 'NONE', #27703, .T. ) ;
#87921=EDGE_CURVE ( 'NONE', #34061, #32906, #71678, .T. ) ;
#87978=B_SPLINE_CURVE_WITH_KNOTS ( 'NONE', 3,
 ( #5009, #54058, #46002, #39508, #87002, #104215, #72382, #79417 ),
 .UNSPECIFIED., .F., .F.,
 ( 4, 2, 2, 4 ),
 ( 0.007886720825438776200, 0.009850969036563999442, 0.01181521724768922268, 0.01574371366993966917 ),
 .UNSPECIFIED. ) ;
#88000=DIRECTION ( 'NONE',  ( -0.000000000000000000, -0.000000000000000000, -1.000000000000000000 ) ) ;
#88090=EDGE_LOOP ( 'NONE', ( #101300, #70314, #17520, #33254 ) ) ;
#88199=VERTEX_POINT ( 'NONE', #10143 ) ;
#88221=CARTESIAN_POINT ( 'NONE',  ( 7.000000000000000000, 0.000000000000000000, -13.00000000000000000 ) ) ;
#88311=EDGE_CURVE ( 'NONE', #104233, #26535, #93627, .T. ) ;
#88362=FACE_OUTER_BOUND ( 'NONE', #90838, .T. ) ;
#88399=CARTESIAN_POINT ( 'NONE',  ( -1.101454001170008912, 14.95253250404441658, -12.16137996778341268 ) ) ;
#88426=AXIS2_PLACEMENT_3D ( 'NONE', #55318, #5719, #105475 ) ;
#88808=CARTESIAN_POINT ( 'NONE',  ( 0.000000000000000000, 0.000000000000000000, -11.82492182392400437 ) ) ;
#88918=ORIENTED_EDGE ( 'NONE', *, *, #23962, .F. ) ;
#89004=CARTESIAN_POINT ( 'NONE',  ( 13.50000000000000355, -6.526560492696110494, -0.8398270946102932566 ) ) ;
#89038=DIRECTION ( 'NONE',  ( -0.000000000000000000, -0.000000000000000000, 1.000000000000000000 ) ) ;
#89072=FACE_OUTER_BOUND ( 'NONE', #43374, .T. ) ;
#89081=CIRCLE ( 'NONE', #80437, 7.000000000000000000 ) ;
#89160=DIRECTION ( 'NONE',  ( 1.000000000000000000, 0.000000000000000000, 0.000000000000000000 ) ) ;
#89177=VECTOR ( 'NONE', #51953, 1000.000000000000000 ) ;
#89213=ORIENTED_EDGE ( 'NONE', *, *, #6513, .T. ) ;
#89262=CARTESIAN_POINT ( 'NONE',  ( 0.000000000000000000, 0.000000000000000000, -11.12471428571428689 ) ) ;
#89264=AXIS2_PLACEMENT_3D ( 'NONE', #91135, #17246, #65778 ) ;
#89274=ORIENTED_EDGE ( 'NONE', *, *, #56251, .T. ) ;
#89313=CARTESIAN_POINT ( 'NONE',  ( 13.50000000000000355, 2.646256834279082870, -0.1392913482116632518 ) ) ;
#89320=ADVANCED_FACE ( 'NONE', ( #11255 ), #10726, .F. ) ;
#89352=CARTESIAN_POINT ( 'NONE',  ( 0.000000000000000000, 0.000000000000000000, -13.00000000000000000 ) ) ;
#89468=CARTESIAN_POINT ( 'NONE',  ( -1.101454001170010244, 14.95253250404441836, -0.8386200322165883181 ) ) ;
#89502=CARTESIAN_POINT ( 'NONE',  ( 0.000000000000000000, 0.000000000000000000, -13.00000000000000000 ) ) ;
#89588=DIRECTION ( 'NONE',  ( -0.000000000000000000, -0.000000000000000000, -1.000000000000000000 ) ) ;
#89664=CARTESIAN_POINT ( 'NONE',  ( 0.000000000000000000, 0.000000000000000000, -1.175078176076019387 ) ) ;
#89694=FACE_OUTER_BOUND ( 'NONE', #46745, .T. ) ;
#89792=DIRECTION ( 'NONE',  ( 0.000000000000000000, 0.000000000000000000, 1.000000000000000000 ) ) ;
#89800=DIRECTION ( 'NONE',  ( 1.000000000000000000, 0.000000000000000000, 0.000000000000000000 ) ) ;
#89930=ORIENTED_EDGE ( 'NONE', *, *, #29665, .T. ) ;
#89945=CYLINDRICAL_SURFACE ( 'NONE', #10882, 7.000000000000000000 ) ;
#90016=CARTESIAN_POINT ( 'NONE',  ( -7.000000000000000000, 8.572527594031471218E-16, -6.724735318933162453 ) ) ;
#90078=CARTESIAN_POINT ( 'NONE',  ( -8.000000000000000000, 0.000000000000000000, -5.575057142857143155 ) ) ;
#90097=SURFACE_SIDE_STYLE ('',( #26466 ) ) ;
#90166=LINE ( 'NONE', #74502, #99891 ) ;
#90295=CARTESIAN_POINT ( 'NONE',  ( 9.036570576874959571, 10.37119081301007917, -12.86120860535742416 ) ) ;
#90377=EDGE_CURVE ( 'NONE', #32846, #71961, #101507, .T. ) ;
#90451=CARTESIAN_POINT ( 'NONE',  ( 13.50000000000000533, -7.794228634059977345, -1.205771365940065953 ) ) ;
#90558=EDGE_CURVE ( 'NONE', #47418, #34348, #23661, .T. ) ;
#90560=FACE_OUTER_BOUND ( 'NONE', #73797, .T. ) ;
#90584=MANIFOLD_SOLID_BREP ( 'ThdSchPat', #51464 ) ;
#90614=AXIS2_PLACEMENT_3D ( 'NONE', #35338, #16053, #52005 ) ;
#90631=CIRCLE ( 'NONE', #99228, 7.000000000000000000 ) ;
#90656=DIRECTION ( 'NONE',  ( 0.000000000000000000, 0.000000000000000000, 1.000000000000000000 ) ) ;
#90701=CARTESIAN_POINT ( 'NONE',  ( -5.724587470723463412E-14, -15.58845726811991561, -1.205771365940065953 ) ) ;
#90710=CARTESIAN_POINT ( 'NONE',  ( 13.50000000000000711, 3.304540750553667028, -12.77799806994943310 ) ) ;
#90805=VECTOR ( 'NONE', #17530, 1000.000000000000000 ) ;
#90808=EDGE_CURVE ( 'NONE', #47413, #64398, #80885, .T. ) ;
#90827=AXIS2_PLACEMENT_3D ( 'NONE', #17426, #15817, #16894 ) ;
#90831=CARTESIAN_POINT ( 'NONE',  ( -7.000000000000000000, 8.572527594031473190E-16, -8.125150395352576993 ) ) ;
#90838=EDGE_LOOP ( 'NONE', ( #67991, #39355, #26715 ) ) ;
#90886=ORIENTED_EDGE ( 'NONE', *, *, #22955, .F. ) ;
#90919=CARTESIAN_POINT ( 'NONE',  ( 0.000000000000000000, 0.000000000000000000, -8.574621033218877031 ) ) ;
#90926=AXIS2_PLACEMENT_3D ( 'NONE', #87489, #33373, #105250 ) ;
#90942=AXIS2_PLACEMENT_3D ( 'NONE', #14608, #89588, #47519 ) ;
#90971=ORIENTED_EDGE ( 'NONE', *, *, #27185, .F. ) ;
#90995=CARTESIAN_POINT ( 'NONE',  ( 9.035703905990981610, -10.37169118567828541, -0.1149164202474967089 ) ) ;
#90998=B_SPLINE_CURVE_WITH_KNOTS ( 'NONE', 3,
 ( #90451, #48905, #81799, #90995, #8987, #82354 ),
 .UNSPECIFIED., .F., .F.,
 ( 4, 2, 4 ),
 ( 2.380729204595406704E-07, 0.003943479449179617714, 0.007886720825438776200 ),
 .UNSPECIFIED. ) ;
#91090=ADVANCED_FACE ( 'NONE', ( #38523 ), #69811, .F. ) ;
#91099=CIRCLE ( 'NONE', #75521, 7.000000000000000000 ) ;
#91135=CARTESIAN_POINT ( 'NONE',  ( 0.000000000000000000, 0.000000000000000000, -12.97459999999999525 ) ) ;
#91137=VERTEX_POINT ( 'NONE', #28872 ) ;
#91150=ADVANCED_FACE ( 'NONE', ( #77372 ), #5223, .T. ) ;
#91192=CARTESIAN_POINT ( 'NONE',  ( 13.50000000000000355, 7.794228634059978233, -1.205771365940065953 ) ) ;
#91199=CARTESIAN_POINT ( 'NONE',  ( 8.000000000000000000, 9.797174393178825657E-16, -3.725171428571429022 ) ) ;
#91226=CARTESIAN_POINT ( 'NONE',  ( -7.000000000000000000, 8.572527594031471218E-16, -13.00000000000000000 ) ) ;
#91302=CARTESIAN_POINT ( 'NONE',  ( 0.000000000000000000, 0.000000000000000000, -13.00000000000000000 ) ) ;
#91415=EDGE_CURVE ( 'NONE', #3555, #44907, #49772, .T. ) ;
#91421=AXIS2_PLACEMENT_3D ( 'NONE', #27564, #11850, #99803 ) ;
#91456=LINE ( 'NONE', #50432, #94803 ) ;
#91520=VERTEX_POINT ( 'NONE', #76167 ) ;
#91593=DIRECTION ( 'NONE',  ( -0.000000000000000000, -0.000000000000000000, -1.000000000000000000 ) ) ;
#91610=ORIENTED_EDGE ( 'NONE', *, *, #57027, .T. ) ;
#91784=ORIENTED_EDGE ( 'NONE', *, *, #26371, .F. ) ;
#91823=CARTESIAN_POINT ( 'NONE',  ( 0.000000000000000000, 0.000000000000000000, 0.000000000000000000 ) ) ;
#91839=DIRECTION ( 'NONE',  ( -1.000000000000000000, 0.000000000000000000, 0.000000000000000000 ) ) ;
#91885=CARTESIAN_POINT ( 'NONE',  ( 7.000000000000000000, 0.000000000000000000, -0.7256075382097185722 ) ) ;
#91888=CIRCLE ( 'NONE', #105653, 7.000000000000000000 ) ;
#91892=DIRECTION ( 'NONE',  ( -1.000000000000000000, 1.776356839400250465E-15, 0.000000000000000000 ) ) ;
#91908=LINE ( 'NONE', #105952, #8645 ) ;
#91936=VERTEX_POINT ( 'NONE', #91192 ) ;
#91965=CONICAL_SURFACE ( 'NONE', #14414, 13.50000000000000178, 1.047197551196596077 ) ;
#92030=DIRECTION ( 'NONE',  ( 0.8191520442889974607, 1.003171929053531649E-16, -0.5735764363510380548 ) ) ;
#92069=ORIENTED_EDGE ( 'NONE', *, *, #22285, .F. ) ;
#92080=FILL_AREA_STYLE ('',( #42465 ) ) ;
#92093=CARTESIAN_POINT ( 'NONE',  ( 7.000000000000000000, 0.000000000000000000, -1.175078176076019387 ) ) ;
#92109=EDGE_CURVE ( 'NONE', #105782, #47418, #74104, .T. ) ;
#92125=EDGE_LOOP ( 'NONE', ( #83810, #40178, #75339, #105889 ) ) ;
#92141=DIRECTION ( 'NONE',  ( 0.000000000000000000, -0.000000000000000000, 1.000000000000000000 ) ) ;
#92296=DIRECTION ( 'NONE',  ( -1.000000000000000000, 0.000000000000000000, 0.000000000000000000 ) ) ;
#92367=CARTESIAN_POINT ( 'NONE',  ( 13.50000000000000355, 7.794228634059934713, -13.00000000000000000 ) ) ;
#92410=CARTESIAN_POINT ( 'NONE',  ( 0.000000000000000000, 0.000000000000000000, -0.01269999999999830292 ) ) ;
#92414=ORIENTED_EDGE ( 'NONE', *, *, #44045, .T. ) ;
#92426=CARTESIAN_POINT ( 'NONE',  ( 0.000000000000000000, 0.000000000000000000, -6.275264681066861527 ) ) ;
#92500=B_SPLINE_CURVE_WITH_KNOTS ( 'NONE', 3,
 ( #61552, #70154, #94446, #20604, #60494, #35154 ),
 .UNSPECIFIED., .F., .F.,
 ( 4, 2, 4 ),
 ( 0.01390592816464533178, 0.01784842065628997748, 0.02179091314793462492 ),
 .UNSPECIFIED. ) ;
#92516=CARTESIAN_POINT ( 'NONE',  ( -8.000000000000000000, 0.000000000000000000, -11.12471428571428689 ) ) ;
#92517=FACE_OUTER_BOUND ( 'NONE', #56551, .T. ) ;
#92543=CARTESIAN_POINT ( 'NONE',  ( -9.035703905990965623, 10.37169118567825343, -12.88508357975252316 ) ) ;
#92566=VECTOR ( 'NONE', #15074, 1000.000000000000000 ) ;
#92572=ADVANCED_FACE ( 'NONE', ( #82731 ), #12215, .F. ) ;
#92647=ORIENTED_EDGE ( 'NONE', *, *, #98287, .F. ) ;
#92662=VERTEX_POINT ( 'NONE', #91885 ) ;
#92694=LINE ( 'NONE', #43613, #3116 ) ;
#92830=( GEOMETRIC_REPRESENTATION_CONTEXT ( 3 ) GLOBAL_UNCERTAINTY_ASSIGNED_CONTEXT ( ( #46405 ) ) GLOBAL_UNIT_ASSIGNED_CONTEXT ( ( #3078, #9557, #68355 ) ) REPRESENTATION_CONTEXT ( 'NONE', 'WORKASPACE' ) );
#92857=EDGE_CURVE ( 'NONE', #44273, #17408, #87978, .T. ) ;
#92886=DIRECTION ( 'NONE',  ( -0.5000000000000011102, -0.8660254037844380415, 0.000000000000000000 ) ) ;
#92973=ORIENTED_EDGE ( 'NONE', *, *, #23528, .F. ) ;
#93089=CARTESIAN_POINT ( 'NONE',  ( 5.600000207755288173, 12.35529564071043040, -13.00000000000000888 ) ) ;
#93098=CONICAL_SURFACE ( 'NONE', #91421, 13.50000000000000178, 1.047197551196596077 ) ;
#93199=EDGE_LOOP ( 'NONE', ( #89930, #67198, #64061, #60891, #31648, #49999 ) ) ;
#93205=CARTESIAN_POINT ( 'NONE',  ( -13.49999999999999645, 0.000000000000000000, -13.00000000000000000 ) ) ;
#93304=DIRECTION ( 'NONE',  ( -1.000000000000000000, 0.000000000000000000, 0.000000000000000000 ) ) ;
#93423=DIRECTION ( 'NONE',  ( 0.000000000000000000, 0.000000000000000000, 1.000000000000000000 ) ) ;
#93520=DIRECTION ( 'NONE',  ( 1.000000000000000000, 0.000000000000000000, 0.000000000000000000 ) ) ;
#93561=DIRECTION ( 'NONE',  ( -1.000000000000000000, 0.000000000000000000, 0.000000000000000000 ) ) ;
#93566=CARTESIAN_POINT ( 'NONE',  ( 0.000000000000000000, 0.000000000000000000, -13.00000000000000000 ) ) ;
#93574=FACE_OUTER_BOUND ( 'NONE', #27086, .T. ) ;
#93601=DIRECTION ( 'NONE',  ( 0.8660254037844380415, 0.5000000000000011102, 0.000000000000000000 ) ) ;
#93627=B_SPLINE_CURVE_WITH_KNOTS ( 'NONE', 3,
 ( #20958, #28493, #46242, #27977, #61377, #37658, #12267, #86719 ),
 .UNSPECIFIED., .F., .F.,
 ( 4, 2, 2, 4 ),
 ( 0.02179091314793461798, 0.02376333058066960879, 0.02573574801340459961, 0.02968058287887458471 ),
 .UNSPECIFIED. ) ;
#93678=LINE ( 'NONE', #61321, #14832 ) ;
#93682=ADVANCED_FACE ( 'NONE', ( #98909 ), #74478, .F. ) ;
#93735=VECTOR ( 'NONE', #39836, 999.9999999999998863 ) ;
#93773=CIRCLE ( 'NONE', #711, 8.000000000000000000 ) ;
#94092=DIRECTION ( 'NONE',  ( -1.000000000000000000, 0.000000000000000000, 0.000000000000000000 ) ) ;
#94206=AXIS2_PLACEMENT_3D ( 'NONE', #8982, #96944, #32769 ) ;
#94207=DIRECTION ( 'NONE',  ( -0.8191520442889974607, 0.000000000000000000, -0.5735764363510380548 ) ) ;
#94217=ADVANCED_FACE ( 'NONE', ( #67516 ), #34647, .F. ) ;
#94317=AXIS2_PLACEMENT_3D ( 'NONE', #89352, #40255, #25167 ) ;
#94405=FACE_OUTER_BOUND ( 'NONE', #41474, .T. ) ;
#94446=CARTESIAN_POINT ( 'NONE',  ( 13.50000000000000355, -5.228219631169433335, -12.46710323223870809 ) ) ;
#94451=EDGE_CURVE ( 'NONE', #50869, #70854, #78527, .T. ) ;
#94552=ORIENTED_EDGE ( 'NONE', *, *, #53118, .F. ) ;
#94635=CARTESIAN_POINT ( 'NONE',  ( 0.000000000000000000, 0.000000000000000000, -4.425378966781146950 ) ) ;
#94664=EDGE_CURVE ( 'NONE', #79700, #60134, #33724, .T. ) ;
#94685=CIRCLE ( 'NONE', #50071, 7.000000000000000000 ) ;
#94766=DIRECTION ( 'NONE',  ( -1.000000000000000000, 0.000000000000000000, 0.000000000000000000 ) ) ;
#94803=VECTOR ( 'NONE', #27823, 1000.000000000000000 ) ;
#94879=ORIENTED_EDGE ( 'NONE', *, *, #63856, .T. ) ;
#94948=EDGE_CURVE ( 'NONE', #1766, #67861, #16059, .T. ) ;
#95022=ORIENTED_EDGE ( 'NONE', *, *, #100169, .T. ) ;
#95159=AXIS2_PLACEMENT_3D ( 'NONE', #54760, #13773, #46685 ) ;
#95172=ADVANCED_FACE ( 'NONE', ( #73211 ), #89945, .F. ) ;
#95262=EDGE_LOOP ( 'NONE', ( #54224, #24719, #51583, #73807 ) ) ;
#95292=AXIS2_PLACEMENT_3D ( 'NONE', #42482, #24734, #75378 ) ;
#95319=ADVANCED_FACE ( 'NONE', ( #89694 ), #31485, .F. ) ;
#95327=AXIS2_PLACEMENT_3D ( 'NONE', #4548, #10505, #94092 ) ;
#95622=AXIS2_PLACEMENT_3D ( 'NONE', #32238, #80760, #73184 ) ;
#95646=AXIS2_PLACEMENT_3D ( 'NONE', #72317, #89038, #105737 ) ;
#95660=CARTESIAN_POINT ( 'NONE',  ( 0.000000000000000000, 0.000000000000000000, -9.274828571428571422 ) ) ;
#95661=ORIENTED_EDGE ( 'NONE', *, *, #24679, .F. ) ;
#95730=CARTESIAN_POINT ( 'NONE',  ( -4.464296094009082339, -13.01099471650159956, -12.88508357975250185 ) ) ;
#95791=DIRECTION ( 'NONE',  ( 0.8191520442889884679, 0.000000000000000000, 0.5735764363510509334 ) ) ;
#95853=EDGE_LOOP ( 'NONE', ( #19552, #26097, #55598, #92973 ) ) ;
#95900=VERTEX_POINT ( 'NONE', #3748 ) ;
#95915=DIRECTION ( 'NONE',  ( -1.000000000000000000, 0.000000000000000000, 0.000000000000000000 ) ) ;
#95982=CONICAL_SURFACE ( 'NONE', #90827, 7.000000000000000000, 0.9599310885968753704 ) ;
#96146=DIRECTION ( 'NONE',  ( -0.000000000000000000, -0.000000000000000000, -1.000000000000000000 ) ) ;
#96203=CARTESIAN_POINT ( 'NONE',  ( 0.000000000000000000, 0.000000000000000000, -13.00000000000000000 ) ) ;
#96206=DIRECTION ( 'NONE',  ( 1.000000000000000000, 0.000000000000000000, 0.000000000000000000 ) ) ;
#96238=VERTEX_POINT ( 'NONE', #42340 ) ;
#96328=DIRECTION ( 'NONE',  ( -1.000000000000000000, 0.000000000000000000, 0.000000000000000000 ) ) ;
#96393=EDGE_LOOP ( 'NONE', ( #65859, #44401, #78698, #95661 ) ) ;
#96621=ADVANCED_FACE ( 'NONE', ( #26357 ), #86686, .F. ) ;
#96626=FACE_OUTER_BOUND ( 'NONE', #83124, .T. ) ;
#96651=LINE ( 'NONE', #32470, #86460 ) ;
#96686=ORIENTED_EDGE ( 'NONE', *, *, #94664, .T. ) ;
#96912=DIRECTION ( 'NONE',  ( -0.000000000000000000, -0.000000000000000000, -1.000000000000000000 ) ) ;
#96913=DIRECTION ( 'NONE',  ( -0.000000000000000000, -0.000000000000000000, -1.000000000000000000 ) ) ;
#96933=FACE_OUTER_BOUND ( 'NONE', #8660, .T. ) ;
#96944=DIRECTION ( 'NONE',  ( -0.000000000000000000, -0.000000000000000000, -1.000000000000000000 ) ) ;
#96998=LINE ( 'NONE', #15004, #93735 ) ;
#97043=FACE_OUTER_BOUND ( 'NONE', #79434, .T. ) ;
#97097=CARTESIAN_POINT ( 'NONE',  ( -13.49999999999999645, 0.000000000000000000, -13.00000000000000000 ) ) ;
#97186=DIRECTION ( 'NONE',  ( 0.000000000000000000, 0.000000000000000000, 1.000000000000000000 ) ) ;
#97410=DIRECTION ( 'NONE',  ( 0.000000000000000000, 0.000000000000000000, 1.000000000000000000 ) ) ;
#97421=DIRECTION ( 'NONE',  ( -1.000000000000000000, 0.000000000000000000, 0.000000000000000000 ) ) ;
#97428=DIRECTION ( 'NONE',  ( -0.8191520442889974607, 0.000000000000000000, -0.5735764363510380548 ) ) ;
#97494=EDGE_CURVE ( 'NONE', #91137, #35268, #91888, .T. ) ;
#97535=ADVANCED_FACE ( 'NONE', ( #88362 ), #91965, .T. ) ;
#97536=DIRECTION ( 'NONE',  ( -0.000000000000000000, -0.000000000000000000, -1.000000000000000000 ) ) ;
#97583=ORIENTED_EDGE ( 'NONE', *, *, #76541, .F. ) ;
#97610=ORIENTED_EDGE ( 'NONE', *, *, #65922, .T. ) ;
#97631=ORIENTED_EDGE ( 'NONE', *, *, #88311, .F. ) ;
#97748=CIRCLE ( 'NONE', #30657, 8.000000000000000000 ) ;
#97838=CARTESIAN_POINT ( 'NONE',  ( -6.750000000000015099, -11.69134295108991495, -13.00000000000000000 ) ) ;
#97872=CONICAL_SURFACE ( 'NONE', #89264, 8.000000000000000000, 0.9599310885968798113 ) ;
#97882=ORIENTED_EDGE ( 'NONE', *, *, #85211, .T. ) ;
#97925=DIRECTION ( 'NONE',  ( -1.000000000000000000, 0.000000000000000000, 0.000000000000000000 ) ) ;
#98013=ORIENTED_EDGE ( 'NONE', *, *, #10031, .F. ) ;
#98014=PLANE ( 'NONE',  #95622 ) ;
#98175=VECTOR ( 'NONE', #14895, 1000.000000000000000 ) ;
#98287=EDGE_CURVE ( 'NONE', #7125, #50869, #4399, .T. ) ;
#98302=AXIS2_PLACEMENT_3D ( 'NONE', #62484, #86245, #45243 ) ;
#98305=ORIENTED_EDGE ( 'NONE', *, *, #64330, .T. ) ;
#98374=ORIENTED_EDGE ( 'NONE', *, *, #52882, .T. ) ;
#98376=EDGE_CURVE ( 'NONE', #74189, #9380, #74784, .T. ) ;
#98426=ORIENTED_EDGE ( 'NONE', *, *, #75508, .T. ) ;
#98633=EDGE_CURVE ( 'NONE', #47418, #105782, #37036, .T. ) ;
#98724=DIRECTION ( 'NONE',  ( 0.000000000000000000, 0.000000000000000000, -1.000000000000000000 ) ) ;
#98811=AXIS2_PLACEMENT_3D ( 'NONE', #96203, #22332, #89160 ) ;
#98823=DIRECTION ( 'NONE',  ( 0.000000000000000000, 0.000000000000000000, 1.000000000000000000 ) ) ;
#98893=DIRECTION ( 'NONE',  ( 0.000000000000000000, 0.000000000000000000, 1.000000000000000000 ) ) ;
#98909=FACE_OUTER_BOUND ( 'NONE', #74337, .T. ) ;
#98952=PRODUCT_DEFINITION_FORMATION_WITH_SPECIFIED_SOURCE ( 'ANY', '', #14592, .NOT_KNOWN. ) ;
#99141=VECTOR ( 'NONE', #58297, 1000.000000000000000 ) ;
#99228=AXIS2_PLACEMENT_3D ( 'NONE', #51769, #60433, #58271 ) ;
#99356=ADVANCED_FACE ( 'NONE', ( #60026 ), #59481, .T. ) ;
#99540=DIRECTION ( 'NONE',  ( -0.8191520442889974607, 0.000000000000000000, -0.5735764363510380548 ) ) ;
#99597=EDGE_LOOP ( 'NONE', ( #102542, #82967, #64283, #41613 ) ) ;
#99617=CARTESIAN_POINT ( 'NONE',  ( -7.000000000000000000, 8.572527594031473190E-16, -11.82492182392400437 ) ) ;
#99642=ORIENTED_EDGE ( 'NONE', *, *, #80092, .T. ) ;
#99659=CARTESIAN_POINT ( 'NONE',  ( -9.601913782316108481, -10.04478976116415012, -0.2204769333331139392 ) ) ;
#99778=FILL_AREA_STYLE_COLOUR ( '', #680 ) ;
#99803=DIRECTION ( 'NONE',  ( 1.000000000000000000, 0.000000000000000000, 0.000000000000000000 ) ) ;
#99841=VERTEX_POINT ( 'NONE', #57587 ) ;
#99891=VECTOR ( 'NONE', #97186, 1000.000000000000000 ) ;
#99936=CARTESIAN_POINT ( 'NONE',  ( 8.000000000000000000, 9.797174393178825657E-16, -0.02540000000000007530 ) ) ;
#99938=ORIENTED_EDGE ( 'NONE', *, *, #98376, .T. ) ;
#99985=ORIENTED_EDGE ( 'NONE', *, *, #68613, .T. ) ;
#100017=LINE ( 'NONE', #59046, #90805 ) ;
#100045=CARTESIAN_POINT ( 'NONE',  ( 13.50000000000000178, 0.000000000000000000, 0.000000000000000000 ) ) ;
#100169=EDGE_CURVE ( 'NONE', #3854, #50065, #34749, .T. ) ;
#100214=ORIENTED_EDGE ( 'NONE', *, *, #7144, .F. ) ;
#100262=DIRECTION ( 'NONE',  ( -0.000000000000000000, -0.000000000000000000, -1.000000000000000000 ) ) ;
#100423=EDGE_LOOP ( 'NONE', ( #79730, #44133, #55057, #41429 ) ) ;
#100438=VERTEX_POINT ( 'NONE', #56165 ) ;
#100637=CARTESIAN_POINT ( 'NONE',  ( 0.000000000000000000, 0.000000000000000000, 0.000000000000000000 ) ) ;
#100665=EDGE_CURVE ( 'NONE', #17408, #68006, #47952, .T. ) ;
#100693=ORIENTED_EDGE ( 'NONE', *, *, #44045, .F. ) ;
#100699=SURFACE_SIDE_STYLE ('',( #26342 ) ) ;
#100762=DIRECTION ( 'NONE',  ( -1.000000000000000000, 0.000000000000000000, 0.000000000000000000 ) ) ;
#100774=ORIENTED_EDGE ( 'NONE', *, *, #86921, .T. ) ;
#100802=CARTESIAN_POINT ( 'NONE',  ( 0.000000000000000000, 0.000000000000000000, -13.00000000000000000 ) ) ;
#101021=EDGE_CURVE ( 'NONE', #52643, #50869, #33932, .T. ) ;
#101048=ORIENTED_EDGE ( 'NONE', *, *, #87673, .F. ) ;
#101060=DIRECTION ( 'NONE',  ( 0.000000000000000000, 0.000000000000000000, 1.000000000000000000 ) ) ;
#101124=ADVANCED_FACE ( 'NONE', ( #35976 ), #71849, .F. ) ;
#101300=ORIENTED_EDGE ( 'NONE', *, *, #43077, .F. ) ;
#101376=CARTESIAN_POINT ( 'NONE',  ( 0.000000000000000000, 0.000000000000000000, -4.874849604647447876 ) ) ;
#101406=CYLINDRICAL_SURFACE ( 'NONE', #54941, 8.000000000000000000 ) ;
#101434=DIRECTION ( 'NONE',  ( -0.8191520442889909104, 0.000000000000000000, -0.5735764363510472696 ) ) ;
#101459=CARTESIAN_POINT ( 'NONE',  ( 7.000000000000000000, 0.000000000000000000, -8.574621033218877031 ) ) ;
#101466=VECTOR ( 'NONE', #102027, 1000.000000000000000 ) ;
#101507=LINE ( 'NONE', #27126, #101466 ) ;
#101552=CONICAL_SURFACE ( 'NONE', #80827, 8.000000000000000000, 0.9599310885968911355 ) ;
#101567=ORIENTED_EDGE ( 'NONE', *, *, #72208, .T. ) ;
#101597=EDGE_CURVE ( 'NONE', #60873, #18742, #100017, .T. ) ;
#101675=ORIENTED_EDGE ( 'NONE', *, *, #15436, .T. ) ;
#101838=ORIENTED_EDGE ( 'NONE', *, *, #43997, .T. ) ;
#101861=CARTESIAN_POINT ( 'NONE',  ( 8.000000000000000000, 9.797174393178825657E-16, -7.424942857142857733 ) ) ;
#101922=EDGE_LOOP ( 'NONE', ( #72355, #30115, #55780 ) ) ;
#101968=CARTESIAN_POINT ( 'NONE',  ( 8.000000000000000000, 0.000000000000000000, 3.469446951953614189E-15 ) ) ;
#102027=DIRECTION ( 'NONE',  ( -0.000000000000000000, -0.000000000000000000, 1.000000000000000000 ) ) ;
#102212=DIRECTION ( 'NONE',  ( 0.5000000000000011102, -0.8660254037844380415, 0.000000000000000000 ) ) ;
#102289=CARTESIAN_POINT ( 'NONE',  ( 7.899999792244755348, -11.02739026146943857, -12.99999999999998934 ) ) ;
#102378=VERTEX_POINT ( 'NONE', #101968 ) ;
#102454=ORIENTED_EDGE ( 'NONE', *, *, #27166, .T. ) ;
#102467=FACE_OUTER_BOUND ( 'NONE', #45564, .T. ) ;
#102542=ORIENTED_EDGE ( 'NONE', *, *, #44750, .F. ) ;
#102555=VECTOR ( 'NONE', #46365, 1000.000000000000000 ) ;
#102627=CIRCLE ( 'NONE', #14760, 7.000000000000000000 ) ;
#102728=VECTOR ( 'NONE', #72282, 1000.000000000000000 ) ;
#102827=ORIENTED_EDGE ( 'NONE', *, *, #7938, .F. ) ;
#102873=ORIENTED_EDGE ( 'NONE', *, *, #69001, .T. ) ;
#102943=AXIS2_PLACEMENT_3D ( 'NONE', #20808, #78978, #69834 ) ;
#102955=AXIS2_PLACEMENT_3D ( 'NONE', #38403, #88000, #54010 ) ;
#102983=ADVANCED_FACE ( 'NONE', ( #61971 ), #37172, .T. ) ;
#102991=ORIENTED_EDGE ( 'NONE', *, *, #94948, .F. ) ;
#103008=CONICAL_SURFACE ( 'NONE', #90926, 7.000000000000000000, 0.9599310885968753704 ) ;
#103501=AXIS2_PLACEMENT_3D ( 'NONE', #90919, #23549, #106011 ) ;
#103634=PRODUCT_DEFINITION ( 'UNKNOWN', '', #98952, #2472 ) ;
#103640=CONICAL_SURFACE ( 'NONE', #105339, 13.50000000000000178, 1.047197551196596077 ) ;
#103810=CARTESIAN_POINT ( 'NONE',  ( -6.158268339717665185E-14, -15.58845726811991739, -11.79422863405993382 ) ) ;
#103855=CARTESIAN_POINT ( 'NONE',  ( -13.50000000000000000, 7.794228634059933825, -1.205771365940051520 ) ) ;
#104139=EDGE_CURVE ( 'NONE', #64475, #30636, #19991, .T. ) ;
#104144=ADVANCED_FACE ( 'NONE', ( #68504 ), #50170, .F. ) ;
#104215=CARTESIAN_POINT ( 'NONE',  ( 2.212097561415789837, -14.31130214556282354, -0.5355294694856076454 ) ) ;
#104233=VERTEX_POINT ( 'NONE', #10248 ) ;
#104327=CARTESIAN_POINT ( 'NONE',  ( 7.000000000000000000, 0.000000000000000000, -4.874849604647447876 ) ) ;
#104448=CIRCLE ( 'NONE', #7974, 8.000000000000000000 ) ;
#104497=ORIENTED_EDGE ( 'NONE', *, *, #101021, .T. ) ;
#104702=LINE ( 'NONE', #79887, #37812 ) ;
#104879=CARTESIAN_POINT ( 'NONE',  ( -13.50000000000000000, 7.794228634059933825, -1.205771365940051520 ) ) ;
#105034=DIRECTION ( 'NONE',  ( 0.5000000000000014433, 0.8660254037844379305, -0.000000000000000000 ) ) ;
#105094=ORIENTED_EDGE ( 'NONE', *, *, #44380, .T. ) ;
#105183=CYLINDRICAL_SURFACE ( 'NONE', #73345, 7.000000000000000000 ) ;
#105246=DIRECTION ( 'NONE',  ( 0.000000000000000000, 0.000000000000000000, -1.000000000000000000 ) ) ;
#105250=DIRECTION ( 'NONE',  ( 1.000000000000000000, 0.000000000000000000, 0.000000000000000000 ) ) ;
#105339=AXIS2_PLACEMENT_3D ( 'NONE', #41041, #98724, #40507 ) ;
#105359=DIRECTION ( 'NONE',  ( -0.8191520442889974607, 0.000000000000000000, -0.5735764363510380548 ) ) ;
#105375=DIRECTION ( 'NONE',  ( 1.000000000000000000, 0.000000000000000000, 0.000000000000000000 ) ) ;
#105448=CARTESIAN_POINT ( 'NONE',  ( 0.000000000000000000, 0.000000000000000000, -0.7256075382097185722 ) ) ;
#105459=DIRECTION ( 'NONE',  ( -0.000000000000000000, -0.000000000000000000, -1.000000000000000000 ) ) ;
#105475=DIRECTION ( 'NONE',  ( -1.000000000000000000, 0.000000000000000000, 0.000000000000000000 ) ) ;
#105536=LINE ( 'NONE', #31677, #2678 ) ;
#105559=ORIENTED_EDGE ( 'NONE', *, *, #57369, .T. ) ;
#105614=ADVANCED_FACE ( 'NONE', ( #9465 ), #281, .F. ) ;
#105653=AXIS2_PLACEMENT_3D ( 'NONE', #79196, #62493, #78130 ) ;
#105737=DIRECTION ( 'NONE',  ( 1.000000000000000000, 0.000000000000000000, 0.000000000000000000 ) ) ;
#105741=MECHANICAL_DESIGN_GEOMETRIC_PRESENTATION_REPRESENTATION('',(#78181),#43772);
#105782=VERTEX_POINT ( 'NONE', #104327 ) ;
#105856=CARTESIAN_POINT ( 'NONE',  ( 7.000000000000000000, 0.000000000000000000, -9.975036109638290682 ) ) ;
#105889=ORIENTED_EDGE ( 'NONE', *, *, #91415, .F. ) ;
#105890=CARTESIAN_POINT ( 'NONE',  ( -7.000000000000000000, 8.572527594031473190E-16, -9.975036109638290682 ) ) ;
#105952=CARTESIAN_POINT ( 'NONE',  ( 6.900000000000000355, 0.000000000000000000, -0.7702282920306786629 ) ) ;
#105978=LINE ( 'NONE', #70978, #21514 ) ;
#106011=DIRECTION ( 'NONE',  ( -1.000000000000000000, 0.000000000000000000, 0.000000000000000000 ) ) ;
#106064=EDGE_CURVE ( 'NONE', #91520, #44907, #96651, .T. ) ;
#106140=CARTESIAN_POINT ( 'NONE',  ( -7.000000000000000000, 8.572527594031471218E-16, -3.024963890361733743 ) ) ;
#106149=DIRECTION ( 'NONE',  ( 0.000000000000000000, 0.000000000000000000, 1.000000000000000000 ) ) ;
#106225=CARTESIAN_POINT ( 'NONE',  ( 8.000000000000000000, 9.797174393178825657E-16, -0.02540000000000007530 ) ) ;
#106279=AXIS2_PLACEMENT_3D ( 'NONE', #64660, #97536, #23697 ) ;
#106284=VECTOR ( 'NONE', #98823, 1000.000000000000000 ) ;
#106300=CARTESIAN_POINT ( 'NONE',  ( 8.000000000000000000, 9.797174393178825657E-16, -5.575057142857143155 ) ) ;
#106408=CARTESIAN_POINT ( 'NONE',  ( 0.000000000000000000, 0.000000000000000000, 0.000000000000000000 ) ) ;
#106440=AXIS2_PLACEMENT_3D ( 'NONE', #43068, #27455, #26920 ) ;
#106499=EDGE_LOOP ( 'NONE', ( #78939, #41513 ) ) ;
#106708=CIRCLE ( 'NONE', #37861, 7.981862520314372489 ) ;
#106742=DIRECTION ( 'NONE',  ( 0.000000000000000000, 0.000000000000000000, 1.000000000000000000 ) ) ;
ENDSEC;
END-ISO-10303-21;
